ISO-10303-21;
HEADER;
FILE_DESCRIPTION (('STEP AP214'),
    '1' );
FILE_NAME ('Drive Spring.step',
    '2026-10-06T09:00:30',
    ( '' ),
    ( '' ),
    'SwSTEP 2.0',
    'SolidWorks 2020',
    '' );
FILE_SCHEMA (( 'AUTOMOTIVE_DESIGN' ));
ENDSEC;

DATA;
#25=CARTESIAN_POINT ( 'NONE',  ( 0.2753640861538455553, 4.598480474408660257, -35.69999999999998863 ) ) ;
#28=CARTESIAN_POINT ( 'NONE',  ( -3.876926306394398836, -0.3768009765330506133, -0.6999999999999992895 ) ) ;
#32=CARTESIAN_POINT ( 'NONE',  ( -5.299969906037439671, -1.662641516789540086, -11.02323088900000769 ) ) ;
#33=CARTESIAN_POINT ( 'NONE',  ( -4.266767049786682087, -2.157590496602210806, -27.02722909260000961 ) ) ;
#40=CARTESIAN_POINT ( 'NONE',  ( 3.800013225884302237, -1.579422177728474708, -17.87122516810000405 ) ) ;
#73=CARTESIAN_POINT ( 'NONE',  ( -3.057389860650357338, 5.459897439232808125, -16.07761783620000173 ) ) ;
#98=CARTESIAN_POINT ( 'NONE',  ( -4.913246905806704312, -2.484498147601009510, -28.96472909259999895 ) ) ;
#133=EDGE_CURVE ( 'NONE', #7914, #29606, #10076, .T. ) ;
#142=CARTESIAN_POINT ( 'NONE',  ( -3.010188847181571870, -5.300177381000955812, -6.685065142700001850 ) ) ;
#147=CARTESIAN_POINT ( 'NONE',  ( -3.665401116828205463, 4.874126016103034864, -20.23064294440001021 ) ) ;
#161=CARTESIAN_POINT ( 'NONE',  ( 0.6138679561251692007, 4.311712124478117580, -29.00600711720001357 ) ) ;
#177=CARTESIAN_POINT ( 'NONE',  ( 0.4017848704880546684, 4.295537307870551658, -35.69999999999999574 ) ) ;
#183=CARTESIAN_POINT ( 'NONE',  ( 3.834994720502944876, -2.823021758520125601, -9.910276792900003073 ) ) ;
#184=CARTESIAN_POINT ( 'NONE',  ( -5.505691776210679400, -0.009179722898969058451, -27.16856466009999238 ) ) ;
#191=CARTESIAN_POINT ( 'NONE',  ( 3.486358836775539594, -2.566383416802844319, -8.972776792899997744 ) ) ;
#221=CARTESIAN_POINT ( 'NONE',  ( 2.051456227667985299, -4.656424856567735304, -0.7000710907721876541 ) ) ;
#226=CARTESIAN_POINT ( 'NONE',  ( -5.990533020055879732, -1.129328118392731950, -16.09949426530000238 ) ) ;
#253=CARTESIAN_POINT ( 'NONE',  ( 4.370697773661016861, 1.580342671372844787, -26.51249766020000109 ) ) ;
#305=CARTESIAN_POINT ( 'NONE',  ( -0.8919388126321509125, 6.008950160842678301, -10.86772091660000150 ) ) ;
#310=CARTESIAN_POINT ( 'NONE',  ( -2.227024806490494946, -3.476280271252722542, -19.20544088820001249 ) ) ;
#322=CARTESIAN_POINT ( 'NONE',  ( 3.499930668453409055, 4.992711500635231836, -29.81106724380000372 ) ) ;
#338=CARTESIAN_POINT ( 'NONE',  ( 0.6569784070868507353, 4.711013504487742587, -35.69999999999999574 ) ) ;
#345=CARTESIAN_POINT ( 'NONE',  ( -3.630162863991666988, -2.403661707492382060, -7.389929326000004295 ) ) ;
#346=CARTESIAN_POINT ( 'NONE',  ( 0.8594151385421661127, 6.036396974313712249, -29.00600711719999936 ) ) ;
#352=CARTESIAN_POINT ( 'NONE',  ( 3.619519562537643065, 2.908736503316577959, -8.354586408000006514 ) ) ;
#382=CARTESIAN_POINT ( 'NONE',  ( -4.278952157217899455, -0.8066629416743122949, -15.59949426530000238 ) ) ;
#410=CARTESIAN_POINT ( 'NONE',  ( 2.193772516446764076, 5.694542648089183423, -26.09462237480000724 ) ) ;
#431=CARTESIAN_POINT ( 'NONE',  ( 2.919161196683367709, -2.910013007151718956, -0.6999999999999992895 ) ) ;
#460=CARTESIAN_POINT ( 'NONE',  ( 3.619519562537647062, 2.908736503316577515, -7.854586408000003850 ) ) ;
#467=CARTESIAN_POINT ( 'NONE',  ( 4.354753084053718304, 0.1085053810021633369, -21.17661200059999871 ) ) ;
#480=CARTESIAN_POINT ( 'NONE',  ( 3.166603938121563377, 4.517215167231739770, -30.21106724380000941 ) ) ;
#493=CARTESIAN_POINT ( 'NONE',  ( 0.5558345775367062869, 4.217921792658845703, -35.70000000000000284 ) ) ;
#497=CARTESIAN_POINT ( 'NONE',  ( -3.505585908281066754, -1.519096937744677245, -0.6999999999999995115 ) ) ;
#500=CARTESIAN_POINT ( 'NONE',  ( 0.5074138422395748638, -6.503547975687064664, -9.393384211799999051 ) ) ;
#501=CARTESIAN_POINT ( 'NONE',  ( -4.702124758411583727, -0.9170245833456597273, -30.15902066320000685 ) ) ;
#509=CARTESIAN_POINT ( 'NONE',  ( 1.213582369797461258, 4.521795443253901148, -2.053410702900000828 ) ) ;
#542=CARTESIAN_POINT ( 'NONE',  ( -2.820898088245517688, -4.403288343584588205, -17.70544088820000539 ) ) ;
#566=CARTESIAN_POINT ( 'NONE',  ( 2.695668638436317543, -3.937035225248731951, -28.07042313650000409 ) ) ;
#585=CARTESIAN_POINT ( 'NONE',  ( 3.633532083198900864, -2.434228036718701027, -0.6999999999999992895 ) ) ;
#608=CARTESIAN_POINT ( 'NONE',  ( 0.3624384587677549341, -4.645391411234346180, -8.893384211800004380 ) ) ;
#616=CARTESIAN_POINT ( 'NONE',  ( 5.403695180783418373, -1.168003237233325553, -24.79036215650000585 ) ) ;
#632=CARTESIAN_POINT ( 'NONE',  ( -2.539202180960155264, -4.449342792696782567, -31.61392233980000199 ) ) ;
#647=CARTESIAN_POINT ( 'NONE',  ( -3.745818880286417851, 2.145659048795447443, -0.6999999999999994005 ) ) ;
#651=CARTESIAN_POINT ( 'NONE',  ( -0.8919388126321509125, 6.008950160842678301, -11.46772091660000470 ) ) ;
#652=CARTESIAN_POINT ( 'NONE',  ( 6.379535387291454640, -1.442012952481606991, -32.78377053309999667 ) ) ;
#658=CARTESIAN_POINT ( 'NONE',  ( -2.308365619037855421, -4.044857084274065429, -30.67642233980000199 ) ) ;
#690=CARTESIAN_POINT ( 'NONE',  ( -5.151963982244392781, -3.152247574024123811, -21.30799200640000279 ) ) ;
#720=SURFACE_STYLE_USAGE ( .BOTH. , #26983 ) ;
#735=CARTESIAN_POINT ( 'NONE',  ( 2.380832905875084116, -3.235963252731846485, -0.6999999999999991784 ) ) ;
#764=CARTESIAN_POINT ( 'NONE',  ( -2.496099253731141943, 5.577352528212363048, -22.73780126169999605 ) ) ;
#779=CARTESIAN_POINT ( 'NONE',  ( -2.448179507319817816, 5.395419651867324973, -32.72635571290000911 ) ) ;
#794=CARTESIAN_POINT ( 'NONE',  ( 2.543356874222871156, 4.353805031640042067, -35.69999999999999574 ) ) ;
#797=CARTESIAN_POINT ( 'NONE',  ( -3.831450486774387265, 1.635689702191160944, -0.6999999999999992895 ) ) ;
#801=CARTESIAN_POINT ( 'NONE',  ( 1.086829820489895848, 5.988658659452708477, -14.62400681849999806 ) ) ;
#802=CARTESIAN_POINT ( 'NONE',  ( -2.448179507325345838, 5.395419651858992971, -30.72635571289999845 ) ) ;
#837=CARTESIAN_POINT ( 'NONE',  ( 0.8228371056950706253, -6.016286819831330845, -0.9731240479999986315 ) ) ;
#838=CARTESIAN_POINT ( 'NONE',  ( -1.058439502263211374, 6.005994971325610443, -19.83583244400000112 ) ) ;
#853=CARTESIAN_POINT ( 'NONE',  ( -1.102325287918849650, -5.983340188646091740, -3.525234013000005717 ) ) ;
#883=CARTESIAN_POINT ( 'NONE',  ( 3.509739097420207621, -2.501532857717466474, -0.6999999999999992895 ) ) ;
#890=MANIFOLD_SOLID_BREP ( 'PartBody', #23115 ) ;
#919=CARTESIAN_POINT ( 'NONE',  ( -2.322678811625146444, -3.635533071076381795, -22.20891267860000795 ) ) ;
#932=CARTESIAN_POINT ( 'NONE',  ( 3.853781668577745734, 2.900580182411895080, -33.29782172560000220 ) ) ;
#952=CARTESIAN_POINT ( 'NONE',  ( -4.383977851963892114, 1.985334855346547966, -0.6999999999999992895 ) ) ;
#956=CARTESIAN_POINT ( 'NONE',  ( 3.550610403408205329, -5.007233058897099021, -12.12388893670000201 ) ) ;
#957=CARTESIAN_POINT ( 'NONE',  ( -5.305719984766040120, 1.510612064730647131, -30.30158078970000091 ) ) ;
#990=CARTESIAN_POINT ( 'NONE',  ( 4.345117593642236820, 2.039387521354418809, -3.416670051700001931 ) ) ;
#991=CARTESIAN_POINT ( 'NONE',  ( 1.391539067366913018, -4.898323207587138128, -20.35785708919999948 ) ) ;
#1007=CARTESIAN_POINT ( 'NONE',  ( 5.782996427689181651, 1.709881257618839356, -17.54190840230000603 ) ) ;
#1035=CARTESIAN_POINT ( 'NONE',  ( 3.309176925312228956, -2.636077854372748774, -0.6999999999999992895 ) ) ;
#1046=EDGE_CURVE ( 'NONE', #23432, #23963, #17250, .T. ) ;
#1054=EDGE_CURVE ( 'NONE', #7914, #21685, #4510, .T. ) ;
#1066=CARTESIAN_POINT ( 'NONE',  ( 4.725722714813314518, -3.873618144263061946, -24.59674734060000745 ) ) ;
#1079=CARTESIAN_POINT ( 'NONE',  ( 2.224662748255027633, -4.232576503996232198, -34.14471934059999825 ) ) ;
#1094=CARTESIAN_POINT ( 'NONE',  ( -3.819171446108351464, 1.704510517422477722, -0.6999999999999991784 ) ) ;
#1095=CARTESIAN_POINT ( 'NONE',  ( -1.392415278799822298, -4.107851135794777342, -0.07563051270000181736 ) ) ;
#1098=CARTESIAN_POINT ( 'NONE',  ( 3.212457031643341399, -4.530353719951508928, -13.12388893670000378 ) ) ;
#1099=CARTESIAN_POINT ( 'NONE',  ( 5.012492089930680628, -1.133010176900860477, -31.84627053310000733 ) ) ;
#1105=CARTESIAN_POINT ( 'NONE',  ( 3.326864889560396499, 2.374768916159259113, -35.37908769470001147 ) ) ;
#1135=CARTESIAN_POINT ( 'NONE',  ( 3.123710955063065065, -2.074832491810036039, 0.04124526979999709742 ) ) ;
#1136=CARTESIAN_POINT ( 'NONE',  ( -5.635022120045706018, 0.7837540840481607152, -18.25159460730000660 ) ) ;
#1151=CARTESIAN_POINT ( 'NONE',  ( -5.082228009654736312, -3.365126390422853220, -6.889929326000007848 ) ) ;
#1177=CARTESIAN_POINT ( 'NONE',  ( -0.7008090670319790938, 4.721317983490957992, -9.930220916600003278 ) ) ;
#1240=CARTESIAN_POINT ( 'NONE',  ( 4.437687981975763307, 3.340062028235890601, -33.36032172560000220 ) ) ;
#1252=CARTESIAN_POINT ( 'NONE',  ( 4.772623561773215783, 2.197494481170958913, -35.69999999999999574 ) ) ;
#1255=CARTESIAN_POINT ( 'NONE',  ( -5.086464543762334145, -0.5886760371733784636, -0.6999999999999992895 ) ) ;
#1256=CARTESIAN_POINT ( 'NONE',  ( 1.213582369797474136, 4.521795443253902924, -1.553410702900004825 ) ) ;
#1261=CARTESIAN_POINT ( 'NONE',  ( -1.302427785971572716, -4.985450142227665360, -13.48772317839999602 ) ) ;
#1262=CARTESIAN_POINT ( 'NONE',  ( -0.4155902256269943806, 5.929468065910143082, -33.89518930509999706 ) ) ;
#1298=CARTESIAN_POINT ( 'NONE',  ( -2.507187057889194381, 3.594686560818127763, -1.627651354100000169 ) ) ;
#1299=CARTESIAN_POINT ( 'NONE',  ( -5.151963982244392781, -3.152247574024123811, -21.90799200640000777 ) ) ;
#1313=CARTESIAN_POINT ( 'NONE',  ( -3.057389860650357338, 5.459897439232808125, -16.67761783620000315 ) ) ;
#1335=CARTESIAN_POINT ( 'NONE',  ( 1.483810035143914297, 4.536549859444123811, -10.13297964829999565 ) ) ;
#1394=CARTESIAN_POINT ( 'NONE',  ( -0.3280975466111886174, 4.681158999438242319, -35.39518930510001127 ) ) ;
#1412=CARTESIAN_POINT ( 'NONE',  ( -3.444986276472465470, -4.029727111321103727, -0.6999999999999992895 ) ) ;
#1413=CARTESIAN_POINT ( 'NONE',  ( -4.325159770583743679, -1.744232581393518666, -0.4971974345000021445 ) ) ;
#1417=CARTESIAN_POINT ( 'NONE',  ( 0.9833222185976336904, 5.418310215658684648, -15.02400681850000019 ) ) ;
#1418=CARTESIAN_POINT ( 'NONE',  ( 5.672553144689285176, -0.9485505809898806540, -35.14517599850000806 ) ) ;
#1448=CARTESIAN_POINT ( 'NONE',  ( 1.212514609374590213, 3.905384712586410068, -35.69999999999998863 ) ) ;
#1457=CARTESIAN_POINT ( 'NONE',  ( 3.691964249065762260, -4.599677940684276933, -4.105321867100004241 ) ) ;
#1458=CARTESIAN_POINT ( 'NONE',  ( -0.4514894588696777289, 4.335480228600245844, -25.88903409329999761 ) ) ;
#1474=CARTESIAN_POINT ( 'NONE',  ( 6.105340317929710992, -0.2107885888489036130, -2.685409721200002320 ) ) ;
#1497=CARTESIAN_POINT ( 'NONE',  ( 3.212457031643341399, -4.530353719951508928, -11.12388893670000378 ) ) ;
#1556=CARTESIAN_POINT ( 'NONE',  ( 2.022420680230021972, -3.847796821814266632, -33.20721934060000535 ) ) ;
#1572=CARTESIAN_POINT ( 'NONE',  ( -3.673964118181757943, -4.849481262180703744, -3.728945369300004753 ) ) ;
#1576=CARTESIAN_POINT ( 'NONE',  ( 1.102985302404366097, 4.375751030832064181, -17.98830441500000177 ) ) ;
#1577=CARTESIAN_POINT ( 'NONE',  ( -4.773116892509256637, 0.6906165796890335606, -33.32033976330000513 ) ) ;
#1589=ORIENTED_EDGE ( 'NONE', *, *, #8530, .T. ) ;
#1609=CARTESIAN_POINT ( 'NONE',  ( 5.763395275750641922, -2.111988417859953504, -5.836105321700000736 ) ) ;
#1610=CARTESIAN_POINT ( 'NONE',  ( -2.496099253731141943, 5.577352528212363048, -22.73780126169999605 ) ) ;
#1627=CARTESIAN_POINT ( 'NONE',  ( 5.195105410215491659, 3.969764343816663210, -23.36727430110000014 ) ) ;
#1649=CARTESIAN_POINT ( 'NONE',  ( 6.482330152203070739, 0.4632910120546396282, -14.64454535870000207 ) ) ;
#1713=ORIENTED_EDGE ( 'NONE', *, *, #10777, .F. ) ;
#1722=CARTESIAN_POINT ( 'NONE',  ( 2.914708617673689606, -3.631324690002112110, -2.605321867100001132 ) ) ;
#1727=CARTESIAN_POINT ( 'NONE',  ( -5.295622588438499534, 1.541709225419852780, -17.30443125760000456 ) ) ;
#1747=CARTESIAN_POINT ( 'NONE',  ( -1.074316293124689015, -5.123231133482405220, -0.7000242870099097070 ) ) ;
#1769=CARTESIAN_POINT ( 'NONE',  ( -4.646804529178781173, -0.2974863596997279203, -4.148838774900000637 ) ) ;
#1770=CARTESIAN_POINT ( 'NONE',  ( -1.961220842241857554, 4.382205557890588743, -21.80030126170000315 ) ) ;
#1788=CARTESIAN_POINT ( 'NONE',  ( 5.307277461536620500, -2.951504967841703131, -26.93037294500000201 ) ) ;
#1810=CARTESIAN_POINT ( 'NONE',  ( -1.302427785971572716, -4.985450142227665360, -11.61272317840000312 ) ) ;
#1858=CARTESIAN_POINT ( 'NONE',  ( 3.436082050571383828, -2.282315740991611719, -36.89625473019999902 ) ) ;
#1876=CARTESIAN_POINT ( 'NONE',  ( -1.949381390262891589, -5.750991590113663676, 0.02436948729999527385 ) ) ;
#1881=CARTESIAN_POINT ( 'NONE',  ( 1.403799475828179766, 5.569137675590418723, -17.65080441500000674 ) ) ;
#1882=CARTESIAN_POINT ( 'NONE',  ( 5.877945039781666381, 1.734296231098907182, -34.93159726780001506 ) ) ;
#1911=CARTESIAN_POINT ( 'NONE',  ( 2.301205939271937950, 3.174620980500392875, -35.69999999999999574 ) ) ;
#1922=CARTESIAN_POINT ( 'NONE',  ( -3.357947603668644199, 3.429589946161242242, -5.506232180600006743 ) ) ;
#1923=CARTESIAN_POINT ( 'NONE',  ( 5.972505199797514486, -1.290950946386169917, -23.79036215650000230 ) ) ;
#1938=CARTESIAN_POINT ( 'NONE',  ( 49.56288048729999218, -32.92067553680000458, 44.14124526979999530 ) ) ;
#1963=CARTESIAN_POINT ( 'NONE',  ( 4.315341029122434335, -4.279276102762477940, -14.46112212870000135 ) ) ;
#2037=CARTESIAN_POINT ( 'NONE',  ( -2.014747437493234816, 4.354226950121528716, -6.794225184300000997 ) ) ;
#2041=CARTESIAN_POINT ( 'NONE',  ( 6.482330152203070739, 0.4632910120546396282, -14.64454535870000207 ) ) ;
#2055=CARTESIAN_POINT ( 'NONE',  ( -2.825020644939634007, -4.425443225455641283, -0.6999999999999992895 ) ) ;
#2069=CARTESIAN_POINT ( 'NONE',  ( 1.612571865511672531, 3.683153181086038952, -35.70000000000000284 ) ) ;
#2076=CARTESIAN_POINT ( 'NONE',  ( -3.052679639724403593, 3.117809041995149411, -5.068732180600003190 ) ) ;
#2077=CARTESIAN_POINT ( 'NONE',  ( 0.09521150875769815447, -4.665041947735804939, -23.91888333260000365 ) ) ;
#2092=CARTESIAN_POINT ( 'NONE',  ( -1.611722395286938170, -6.291674585240492057, -27.54882611459999353 ) ) ;
#2110=CARTESIAN_POINT ( 'NONE',  ( 3.636072258898020770, -3.161266087984368145, -0.6999085127358649627 ) ) ;
#2113=CARTESIAN_POINT ( 'NONE',  ( 1.526412975746457290, -4.524531468931415112, -14.32664732020000287 ) ) ;
#2191=CARTESIAN_POINT ( 'NONE',  ( -3.010188847181571870, -5.300177381000955812, -6.085065142700004870 ) ) ;
#2197=CARTESIAN_POINT ( 'NONE',  ( 1.002713911322304696, 3.977955482547951505, -17.05080441500000177 ) ) ;
#2226=CARTESIAN_POINT ( 'NONE',  ( 1.438618989620732647, 4.694460304239756354, -35.70000000000000284 ) ) ;
#2236=CARTESIAN_POINT ( 'NONE',  ( 6.086077541567210147, 0.7980478301550381071, -5.626979598400000171 ) ) ;
#2237=CARTESIAN_POINT ( 'NONE',  ( -3.052438874386664835, 3.509528713898347974, -28.58728588869999143 ) ) ;
#2244=CARTESIAN_POINT ( 'NONE',  ( -4.430040892179083478, 1.363067613765873931, -22.32289663399999924 ) ) ;
#2276=CARTESIAN_POINT ( 'NONE',  ( -3.283272085064022239, -5.616145207998583189, -15.08182079290000566 ) ) ;
#2332=CARTESIAN_POINT ( 'NONE',  ( 5.318140750225764712, 1.569125161463077900, -36.53159726779999517 ) ) ;
#2347=CARTESIAN_POINT ( 'NONE',  ( -1.831588579526997940, 3.958388136463042439, -7.731725184300007214 ) ) ;
#2352=CARTESIAN_POINT ( 'NONE',  ( 3.931047123110464891, -1.876836795983964912, -21.38180150030001059 ) ) ;
#2382=CARTESIAN_POINT ( 'NONE',  ( 0.5467022973628515858, 4.692255042463733261, -35.69999999999998863 ) ) ;
#2388=CARTESIAN_POINT ( 'NONE',  ( 0.5074138422395748638, -6.503547975687064664, -9.993384211800002248 ) ) ;
#2389=CARTESIAN_POINT ( 'NONE',  ( -1.611722395286938170, -6.291674585240492057, -26.94882611460000632 ) ) ;
#2393=CARTESIAN_POINT ( 'NONE',  ( 2.326244606069574505, 3.379075471592551949, -17.21259163650000446 ) ) ;
#2421=CARTESIAN_POINT ( 'NONE',  ( 3.030289999311443161, -3.940603520075978139, -0.6999848558563146472 ) ) ;
#2424=CARTESIAN_POINT ( 'NONE',  ( -3.283272085064022239, -5.616145207998583189, -15.68182079290000175 ) ) ;
#2452=CARTESIAN_POINT ( 'NONE',  ( -1.151230282303593366, -4.494053275198268693, -27.54882611460000774 ) ) ;
#2465=CARTESIAN_POINT ( 'NONE',  ( 4.334836395473461224, -2.879286697580460519, -35.69999999999999574 ) ) ;
#2497=CARTESIAN_POINT ( 'NONE',  ( 3.530284718056032833, 5.524446756132658898, -5.200967428500000267 ) ) ;
#2502=CARTESIAN_POINT ( 'NONE',  ( 3.791027721911684800, -3.577548591872723449, -19.03565261000001385 ) ) ;
#2516=CARTESIAN_POINT ( 'NONE',  ( -4.273414424137721213, 4.913340199448848367, -29.18728588869999641 ) ) ;
#2530=CARTESIAN_POINT ( 'NONE',  ( 0.6438416807965144928, 4.176741662662551313, -35.69999999999999574 ) ) ;
#2537=CARTESIAN_POINT ( 'NONE',  ( -6.277996069133942925, 1.777976852108807737, -7.310827254900003069 ) ) ;
#2538=CARTESIAN_POINT ( 'NONE',  ( -4.273414424137721213, 4.913340199448848367, -28.58728588869999143 ) ) ;
#2546=CARTESIAN_POINT ( 'NONE',  ( 2.914708617673698932, -3.631324690002109445, -3.105321867099997135 ) ) ;
#2574=CARTESIAN_POINT ( 'NONE',  ( 5.782996427689181651, 1.709881257618839356, -17.54190840230000603 ) ) ;
#2599=CARTESIAN_POINT ( 'NONE',  ( -0.4514894588696835021, 4.335480228600247621, -26.38903409329999761 ) ) ;
#2627=CARTESIAN_POINT ( 'NONE',  ( 0.000000000000000000, 0.000000000000000000, 0.000000000000000000 ) ) ;
#2643=CARTESIAN_POINT ( 'NONE',  ( -5.082228009654736312, -3.365126390422853220, -6.889929326000007848 ) ) ;
#2648=CARTESIAN_POINT ( 'NONE',  ( -3.331422745097509797, -2.438398348906448021, -19.37254627010001329 ) ) ;
#2664=CARTESIAN_POINT ( 'NONE',  ( 4.420334067734101424, -4.199682076162645217, -30.65126389020000985 ) ) ;
#2680=CARTESIAN_POINT ( 'NONE',  ( 0.7542811793706193368, 4.720842771144411643, -35.70000000000000284 ) ) ;
#2685=CARTESIAN_POINT ( 'NONE',  ( -3.099128499470596321, -3.102542665468454253, -9.813991631000003935 ) ) ;
#2686=CARTESIAN_POINT ( 'NONE',  ( 4.634019325638258024, 0.4639887426745141208, -29.13116556700001070 ) ) ;
#2693=CARTESIAN_POINT ( 'NONE',  ( 4.354753084053725409, 0.1085053810021691101, -20.67661200060000226 ) ) ;
#2729=CARTESIAN_POINT ( 'NONE',  ( 2.326244606069572285, 3.379075471592549729, -16.71259163650000090 ) ) ;
#2757=CARTESIAN_POINT ( 'NONE',  ( 0.09521150875769815447, -4.665041947735804939, -24.91888333260000721 ) ) ;
#2802=CARTESIAN_POINT ( 'NONE',  ( 4.294959833232216972, -2.194189917041240445, -10.97724735219999914 ) ) ;
#2807=CARTESIAN_POINT ( 'NONE',  ( -3.117834729128555971, -4.866792379758847709, -19.30544088820000681 ) ) ;
#2820=CARTESIAN_POINT ( 'NONE',  ( -6.085238278930475531, -0.01014600953121863602, -28.76856466009999735 ) ) ;
#2833=CARTESIAN_POINT ( 'NONE',  ( 0.3516186674615833230, 4.635787241539998327, -35.69999999999998863 ) ) ;
#2837=CARTESIAN_POINT ( 'NONE',  ( 4.262818619062177738, -0.7545854518158033875, -9.271482634700010550 ) ) ;
#2838=CARTESIAN_POINT ( 'NONE',  ( 1.723678405763061194, 4.474283509182772178, -25.15712237480000013 ) ) ;
#2847=CARTESIAN_POINT ( 'NONE',  ( 3.082386449366550263, -3.056625787687238471, -15.06112212870000455 ) ) ;
#2878=CARTESIAN_POINT ( 'NONE',  ( 0.7420639427752478978, -6.011517603930927045, -18.37054674910000429 ) ) ;
#2905=CARTESIAN_POINT ( 'NONE',  ( 5.536217179945332134, 2.001767383715431503, -27.51249766020000465 ) ) ;
#2923=CARTESIAN_POINT ( 'NONE',  ( 3.056196190786856448, -2.814750735090191025, -0.6999999999999992895 ) ) ;
#2952=CARTESIAN_POINT ( 'NONE',  ( -3.099128499470596765, -3.102542665468459138, -9.313991631000007487 ) ) ;
#2958=CARTESIAN_POINT ( 'NONE',  ( -0.9576357401321299312, 5.433995450232204760, -20.83583244400000467 ) ) ;
#2976=CARTESIAN_POINT ( 'NONE',  ( 2.039164074698236906, -5.746172002732055084, -30.25632401680000783 ) ) ;
#2992=CARTESIAN_POINT ( 'NONE',  ( -3.738201190122705686, 2.321745386530837063, -0.6999999999999992895 ) ) ;
#2996=CARTESIAN_POINT ( 'NONE',  ( -3.950034095761355335, 2.484763540022569384, -10.44547590280000371 ) ) ;
#2997=CARTESIAN_POINT ( 'NONE',  ( 4.556810990865953315, -1.030009251744165688, -32.78377053309999667 ) ) ;
#3003=CARTESIAN_POINT ( 'NONE',  ( -3.554763430470064822, 2.566410659217317924, -34.46696136359999940 ) ) ;
#3030=CARTESIAN_POINT ( 'NONE',  ( -0.7560282158644084927, 4.289996408053712962, -19.83583244400000112 ) ) ;
#3054=CARTESIAN_POINT ( 'NONE',  ( -1.266353310550808464, -4.943458602710906646, -28.48632611460000419 ) ) ;
#3072=CARTESIAN_POINT ( 'NONE',  ( 2.746047774209056325, -3.024004467141764962, -0.6999999999999992895 ) ) ;
#3106=CARTESIAN_POINT ( 'NONE',  ( -6.202057249109299342, 1.908294659314309305, -22.32289663399999924 ) ) ;
#3120=CARTESIAN_POINT ( 'NONE',  ( -4.702124758411583727, -0.9170245833456597273, -32.03402066320000330 ) ) ;
#3138=CARTESIAN_POINT ( 'NONE',  ( -4.687286842521976027, -2.264969778146401769, -0.6999999999999992895 ) ) ;
#3143=CARTESIAN_POINT ( 'NONE',  ( -4.363437395929419260, 0.1294788321584625090, -13.18304957890000573 ) ) ;
#3144=CARTESIAN_POINT ( 'NONE',  ( -5.414567903583902719, -1.055967702048432599, -30.09652066319999975 ) ) ;
#3180=CARTESIAN_POINT ( 'NONE',  ( 3.112737406813101515, -4.802415649948616583, -0.7659393883000034098 ) ) ;
#3181=CARTESIAN_POINT ( 'NONE',  ( -3.664565019602479268, -2.682238183793479447, -17.93504627010000618 ) ) ;
#3213=( NAMED_UNIT ( * ) PLANE_ANGLE_UNIT ( ) SI_UNIT ( $, .RADIAN. ) );
#3214=CARTESIAN_POINT ( 'NONE',  ( -2.017871889752692383, -3.161030873707806332, -0.6999999999999992895 ) ) ;
#3260=CARTESIAN_POINT ( 'NONE',  ( -4.430040892179083478, 1.363067613765873931, -22.32289663399999924 ) ) ;
#3274=CARTESIAN_POINT ( 'NONE',  ( -4.339197174995631734, 0.6278332542688225271, -34.25783976329999092 ) ) ;
#3288=CARTESIAN_POINT ( 'NONE',  ( 2.073932621141414412, 4.546060023457436650, -35.70000000000000284 ) ) ;
#3292=CARTESIAN_POINT ( 'NONE',  ( -4.376928212848416599, 1.994761680063780407, -0.6999999999999992895 ) ) ;
#3297=CARTESIAN_POINT ( 'NONE',  ( -3.941349475653395551, -1.876729865818549392, -12.97655742010000246 ) ) ;
#3298=CARTESIAN_POINT ( 'NONE',  ( -5.864216825196034932, 1.669623860970033347, -30.70158078970000659 ) ) ;
#3303=CARTESIAN_POINT ( 'NONE',  ( 2.499950477468926291, 3.566222500441432075, -29.21106724380000230 ) ) ;
#3330=CARTESIAN_POINT ( 'NONE',  ( 3.112737406813101515, -4.802415649948616583, -0.1659393883000001568 ) ) ;
#3331=CARTESIAN_POINT ( 'NONE',  ( -2.618143654921863295, 3.481518582925488658, -19.63064294430000345 ) ) ;
#3412=CARTESIAN_POINT ( 'NONE',  ( 1.602378319964792297, -5.640493390528545703, -22.29535708920000303 ) ) ;
#3425=CARTESIAN_POINT ( 'NONE',  ( 5.012492089925147276, -1.133010176909191591, -33.72127053310000377 ) ) ;
#3437=CARTESIAN_POINT ( 'NONE',  ( 5.273012595518953738, 0.3921573701267448420, -35.69999999999999574 ) ) ;
#3441=CARTESIAN_POINT ( 'NONE',  ( -4.820115942865387915, 1.170356313244571345, -0.6999999999999992895 ) ) ;
#3442=CARTESIAN_POINT ( 'NONE',  ( 3.112737406813101515, -4.802415649948616583, 0.4340606116999962127 ) ) ;
#3446=CARTESIAN_POINT ( 'NONE',  ( 1.888485499342153151, 5.773790730162923879, -11.67047964830000062 ) ) ;
#3447=CARTESIAN_POINT ( 'NONE',  ( -5.984522419796141079, -1.167122196978044535, -30.49652066320000898 ) ) ;
#3453=CARTESIAN_POINT ( 'NONE',  ( 2.315582734148106780, 3.377836756897303783, -35.21970670790000923 ) ) ;
#3485=CARTESIAN_POINT ( 'NONE',  ( -1.392415278799822298, -4.107851135794777342, -1.075630512700001651 ) ) ;
#3486=CARTESIAN_POINT ( 'NONE',  ( -6.228182343209494043, 0.8662545139425728014, -19.25159460730001371 ) ) ;
#3502=CARTESIAN_POINT ( 'NONE',  ( -5.990533020055879732, -1.129328118392731950, -16.09949426530000238 ) ) ;
#3519=FILL_AREA_STYLE_COLOUR ( '', #8895 ) ;
#3524=CARTESIAN_POINT ( 'NONE',  ( -5.003376521275985311, 3.147367150682292447, -9.445475902800000156 ) ) ;
#3569=CARTESIAN_POINT ( 'NONE',  ( 0.1332961122732720383, -6.531058726825651028, -24.41888333260000365 ) ) ;
#3581=CARTESIAN_POINT ( 'NONE',  ( -6.074876045044606876, 0.8789665559579967757, -34.85783976329999234 ) ) ;
#3596=CARTESIAN_POINT ( 'NONE',  ( -3.745457574878203300, 2.149009913884074141, -0.6999999999999994005 ) ) ;
#3597=CARTESIAN_POINT ( 'NONE',  ( 4.797053106898050423, -0.1656196055093784036, -1.747909721200001210 ) ) ;
#3601=CARTESIAN_POINT ( 'NONE',  ( -4.335484423225056005, -2.064402852395420318, -13.91405742009999358 ) ) ;
#3602=CARTESIAN_POINT ( 'NONE',  ( -4.188726303739433554, 1.192588472141202560, -31.30158078970000801 ) ) ;
#3607=CARTESIAN_POINT ( 'NONE',  ( 0.2309929099465271585, 4.358477053493584386, -22.94418644579999977 ) ) ;
#3639=CARTESIAN_POINT ( 'NONE',  ( 3.436082050571401147, -2.282315740991585962, -0.8962547302000020144 ) ) ;
#3640=CARTESIAN_POINT ( 'NONE',  ( 2.949882002856666130, 3.605460750137340131, -19.75622222230000702 ) ) ;
#3656=CARTESIAN_POINT ( 'NONE',  ( -0.8919388126321509125, 6.008950160842678301, -10.86772091660000150 ) ) ;
#3682=CARTESIAN_POINT ( 'NONE',  ( -0.8919388126321509125, 6.008950160842678301, -10.26772091660000541 ) ) ;
#3727=CARTESIAN_POINT ( 'NONE',  ( 3.690858198475444940, -2.451543251927155165, -0.7069547853999700315 ) ) ;
#3750=CARTESIAN_POINT ( 'NONE',  ( 4.556810990865953315, -1.030009251744165688, -32.78377053309999667 ) ) ;
#3766=CARTESIAN_POINT ( 'NONE',  ( 6.105340317846409626, -0.2107885887935728730, -2.085409721200005784 ) ) ;
#3771=CARTESIAN_POINT ( 'NONE',  ( 1.086829820489895848, 5.988658659452708477, -14.02400681850000197 ) ) ;
#3772=CARTESIAN_POINT ( 'NONE',  ( 4.457006042266220547, -0.7452897422089094226, -34.80767599850000238 ) ) ;
#3803=CARTESIAN_POINT ( 'NONE',  ( 2.456693329403278447, 3.027921411505207328, -35.69999999999999574 ) ) ;
#3811=CARTESIAN_POINT ( 'NONE',  ( 4.360957369889326252, -0.1505632777267507105, -2.685409721200002320 ) ) ;
#3812=CARTESIAN_POINT ( 'NONE',  ( 3.713067847428462631, -3.043557113396612390, -23.05924734060000603 ) ) ;
#3827=CARTESIAN_POINT ( 'NONE',  ( -5.857861475075242019, -1.837656413297739766, -10.02323088899999881 ) ) ;
#3848=CARTESIAN_POINT ( 'NONE',  ( 4.741512700999319208, 1.965332957690412385, -10.55511350020000094 ) ) ;
#3905=CARTESIAN_POINT ( 'NONE',  ( 5.877945039781666381, 1.734296231098907182, -35.53159726780000227 ) ) ;
#3922=CARTESIAN_POINT ( 'NONE',  ( -0.7873752056533345201, -4.273814420472608511, -3.525234013000005717 ) ) ;
#3927=CARTESIAN_POINT ( 'NONE',  ( 3.082386449366550263, -3.056625787687238471, -15.06112212870000455 ) ) ;
#3928=CARTESIAN_POINT ( 'NONE',  ( -0.3280975466111932248, 4.681158999438244983, -34.89518930510001127 ) ) ;
#3945=CARTESIAN_POINT ( 'NONE',  ( -0.8162763503540674259, -5.159721775937600619, -0.7000226544067725820 ) ) ;
#3963=CARTESIAN_POINT ( 'NONE',  ( 6.086077541567210147, 0.7980478301550381071, -6.226979598400003368 ) ) ;
#3964=CARTESIAN_POINT ( 'NONE',  ( 0.3233900739386466605, 6.101867874933233793, -22.34418644579999480 ) ) ;
#3966=APPLICATION_CONTEXT ( 'automotive_design' ) ;
#3972=CARTESIAN_POINT ( 'NONE',  ( -3.044741706671135084, -2.260426224203013312, -0.8737437980999990250 ) ) ;
#3981=CARTESIAN_POINT ( 'NONE',  ( 2.246931792487971702, -6.149078805931920577, -6.260585232200001293 ) ) ;
#3989=VERTEX_POINT ( 'NONE', #17605 ) ;
#4005=CARTESIAN_POINT ( 'NONE',  ( 2.536150288113629081, -3.576595042060319862, -11.62388893670000733 ) ) ;
#4079=CARTESIAN_POINT ( 'NONE',  ( -6.055223678858003389, -2.441925613954294860, -0.3971974345000003903 ) ) ;
#4083=CARTESIAN_POINT ( 'NONE',  ( -4.278952157217901231, -0.8066629416743145153, -16.09949426530000238 ) ) ;
#4119=CARTESIAN_POINT ( 'NONE',  ( -5.885952403586735215, -0.3768160556055083488, -5.148838774900003301 ) ) ;
#4120=CARTESIAN_POINT ( 'NONE',  ( 5.403695180783418373, -1.168003237233325553, -22.79036215650000941 ) ) ;
#4135=CARTESIAN_POINT ( 'NONE',  ( -1.006352433577557770, 6.195109836679514537, -34.84333403589999278 ) ) ;
#4161=CARTESIAN_POINT ( 'NONE',  ( -4.101794773660127902, 5.071170285176791914, -13.60352819870000474 ) ) ;
#4203=( GEOMETRIC_REPRESENTATION_CONTEXT ( 3 ) GLOBAL_UNCERTAINTY_ASSIGNED_CONTEXT ( ( #4655 ) ) GLOBAL_UNIT_ASSIGNED_CONTEXT ( ( #10637, #22750, #17555 ) ) REPRESENTATION_CONTEXT ( 'NONE', 'WORKASPACE' ) );
#4235=CARTESIAN_POINT ( 'NONE',  ( -2.624260084387257219, -3.463915187244964056, -3.728945369300004753 ) ) ;
#4239=CARTESIAN_POINT ( 'NONE',  ( 1.403799475828179766, 5.569137675590418723, -17.05080441500000177 ) ) ;
#4240=CARTESIAN_POINT ( 'NONE',  ( 5.132309988016721114, -0.8582124304006011339, -34.74517599850000948 ) ) ;
#4273=CARTESIAN_POINT ( 'NONE',  ( 2.748504964697384700, 2.712961263263990119, -35.69999999999999574 ) ) ;
#4279=CARTESIAN_POINT ( 'NONE',  ( 2.521631941452528558, 3.946033397249446573, -5.700967428500005596 ) ) ;
#4281=CARTESIAN_POINT ( 'NONE',  ( -4.215937884789293655, -1.105999120962562809, -25.04656121680000425 ) ) ;
#4299=CARTESIAN_POINT ( 'NONE',  ( 2.635706879431563898, 5.544231365240147369, -32.15113063600000487 ) ) ;
#4319=CARTESIAN_POINT ( 'NONE',  ( -6.108812354267502798, 0.1812703649498176306, -13.18304957890000040 ) ) ;
#4389=CARTESIAN_POINT ( 'NONE',  ( 4.116710911288348207, -1.508563155650262111, -5.336105321700006066 ) ) ;
#4393=CARTESIAN_POINT ( 'NONE',  ( -4.598830142556993295, 1.338852748371190282, -17.24193125760000100 ) ) ;
#4394=CARTESIAN_POINT ( 'NONE',  ( -3.500772897184936561, -3.093025330206538470, -33.83447003410000775 ) ) ;
#4412=CARTESIAN_POINT ( 'NONE',  ( 1.229305342267849932, -4.993942504622491896, -0.7000000457190377334 ) ) ;
#4425=CARTESIAN_POINT ( 'NONE',  ( 1.930846921697753960, 3.466634617185091027, -35.69999999999999574 ) ) ;
#4433=CARTESIAN_POINT ( 'NONE',  ( 4.116710911288348207, -1.508563155650262111, -6.336105321700005177 ) ) ;
#4434=CARTESIAN_POINT ( 'NONE',  ( 0.1332961122732720383, -6.531058726825651028, -24.41888333260000365 ) ) ;
#4453=CARTESIAN_POINT ( 'NONE',  ( -5.367600138795724618, 3.713494282866228069, -25.46779765530001072 ) ) ;
#4470=CARTESIAN_POINT ( 'NONE',  ( 3.463630677558556581, -3.438880230788124326, -0.6996960715771658457 ) ) ;
#4474=CARTESIAN_POINT ( 'NONE',  ( 4.630235822890134578, 0.3309221515414850767, -14.64454535870000207 ) ) ;
#4510=B_SPLINE_CURVE_WITH_KNOTS ( 'NONE', 3,
 ( #16881, #21768, #30906, #4785, #23674, #4929, #2110, #6823, #11701, #6983, #14537, #26337, #16572, #28835, #4470, #12159, #26179, #26030, #14383, #2421, #12010, #21617, #9647, #19249, #7294, #26485, #24131, #221, #21148, #30744, #9174, #15737, #6140, #23301, #4412, #14016, #22989, #8970, #25823, #18413, #16210, #25350, #11648, #30692, #20937, #20778, #25508, #3945, #23621, #18247, #11031, #30847, #1747, #28322, #23465, #13538, #2055 ),
 .UNSPECIFIED., .F., .F.,
 ( 4, 2, 2, 2, 1, 1, 1, 2, 2, 2, 2, 1, 1, 1, 2, 2, 2, 2, 2, 1, 1, 1, 2, 2, 2, 2, 2, 1, 1, 1, 1, 2, 2, 2, 4 ),
 ( 0.000000000000000000, 0.06250000000000456579, 0.09375000000000681399, 0.1093750000000078826, 0.1171875000000085071, 0.1210937500000087846, 0.1230468750000089095, 0.1240234375000090206, 0.1250000000000091316, 0.1875000000000074107, 0.2187500000000065781, 0.2343750000000061062, 0.2421875000000059952, 0.2460937500000059674, 0.2480468750000059397, 0.2500000000000058842, 0.3750000000000114353, 0.4375000000000142664, 0.4687500000000157097, 0.4843750000000163758, 0.4921875000000166533, 0.4960937500000167644, 0.4980468750000168199, 0.5000000000000168754, 0.6250000000000124345, 0.6875000000000101030, 0.7187500000000089928, 0.7343750000000083267, 0.7421875000000079936, 0.7460937500000078826, 0.7480468750000077716, 0.7490234375000077716, 0.7500000000000076605, 0.8750000000000038858, 1.000000000000000000 ),
 .UNSPECIFIED. ) ;
#4544=CARTESIAN_POINT ( 'NONE',  ( 4.347198243976411192, 0.5700341643805815206, -5.126979598399998395 ) ) ;
#4549=CARTESIAN_POINT ( 'NONE',  ( 4.813350086082918367, -2.000601425115993148, -18.87122516810000405 ) ) ;
#4575=CARTESIAN_POINT ( 'NONE',  ( 0.5265107913985979105, 4.688092003840730548, -35.69999999999999574 ) ) ;
#4580=CARTESIAN_POINT ( 'NONE',  ( -5.082228009654736312, -3.365126390422853220, -6.889929326000007848 ) ) ;
#4581=CARTESIAN_POINT ( 'NONE',  ( 3.790912472548403578, -2.108217834232220422, -26.93037294500000201 ) ) ;
#4586=CARTESIAN_POINT ( 'NONE',  ( 3.931047123110473329, -1.876836795983962469, -20.88180150029999993 ) ) ;
#4619=PRODUCT_DEFINITION ( 'UNKNOWN', '', #6817, #30121 ) ;
#4620=CARTESIAN_POINT ( 'NONE',  ( 1.002713911322304696, 3.977955482547951505, -17.05080441500000177 ) ) ;
#4655=UNCERTAINTY_MEASURE_WITH_UNIT (LENGTH_MEASURE( 1.000000000000000082E-05 ), #10637, 'distance_accuracy_value', 'NONE');
#4696=CARTESIAN_POINT ( 'NONE',  ( -1.814319851916122772, 5.833166587536846137, -4.174955258300000693 ) ) ;
#4701=CARTESIAN_POINT ( 'NONE',  ( 4.324151835433248436, -2.064520475586355985, -21.81930150030000348 ) ) ;
#4735=CARTESIAN_POINT ( 'NONE',  ( 0.3409666413401617469, 4.631268320286548779, -35.69999999999999574 ) ) ;
#4737=CARTESIAN_POINT ( 'NONE',  ( -2.446005382334546230, -2.858172524253452806, -0.6999999999999992895 ) ) ;
#4746=CARTESIAN_POINT ( 'NONE',  ( -4.484282906631567478, 1.269983465873030015, -7.310827254900003069 ) ) ;
#4747=CARTESIAN_POINT ( 'NONE',  ( 4.801822465207213675, -2.670409256638542672, -25.93037294500000201 ) ) ;
#4755=CARTESIAN_POINT ( 'NONE',  ( 4.130711734062736618, 1.221343755424965316, -17.54190840230000248 ) ) ;
#4763=CARTESIAN_POINT ( 'NONE',  ( -5.984522419796141079, -1.167122196978044535, -31.09652066320001040 ) ) ;
#4785=CARTESIAN_POINT ( 'NONE',  ( 3.750083858941618775, -2.929025673886469505, -0.7000271815399211617 ) ) ;
#4789=CARTESIAN_POINT ( 'NONE',  ( 4.190083271568243894, -3.954132654168471817, -17.43565260999999822 ) ) ;
#4816=CARTESIAN_POINT ( 'NONE',  ( -1.611722395286938170, -6.291674585240492057, -27.54882611459999353 ) ) ;
#4858=CARTESIAN_POINT ( 'NONE',  ( -6.277996069133942925, 1.777976852108807737, -7.310827254900003069 ) ) ;
#4863=CARTESIAN_POINT ( 'NONE',  ( -3.665401116828205463, 4.874126016103034864, -19.63064294430000345 ) ) ;
#4874=CARTESIAN_POINT ( 'NONE',  ( 0.6752547517502489605, 4.742883336923179094, -29.94350711720000291 ) ) ;
#4890=CARTESIAN_POINT ( 'NONE',  ( 1.161059139478890501, 3.931710991834906466, -35.69999999999999574 ) ) ;
#4898=CARTESIAN_POINT ( 'NONE',  ( -5.003376521275985311, 3.147367150682292447, -11.44547590280000193 ) ) ;
#4899=CARTESIAN_POINT ( 'NONE',  ( -3.878879136156900387, -1.961445906012333928, -27.46472909260000961 ) ) ;
#4904=CARTESIAN_POINT ( 'NONE',  ( -4.169787897409099386, -0.4107988151082903050, -1.146254077200002719 ) ) ;
#4929=CARTESIAN_POINT ( 'NONE',  ( 3.658248740575405833, -3.120266197651133222, -0.6999349691374636695 ) ) ;
#4932=CARTESIAN_POINT ( 'NONE',  ( -5.990533020055879732, -1.129328118392731950, -15.49949426529999919 ) ) ;
#4957=CARTESIAN_POINT ( 'NONE',  ( 3.790912472548402246, -2.108217834232220866, -27.43037294500001266 ) ) ;
#5005=CARTESIAN_POINT ( 'NONE',  ( 1.604951280288046567, -4.392199147046019547, -5.760585232199999517 ) ) ;
#5010=CARTESIAN_POINT ( 'NONE',  ( 4.190083271568243894, -3.954132654168471817, -18.03565260999999964 ) ) ;
#5025=CARTESIAN_POINT ( 'NONE',  ( -3.231711866632715147, -5.662799918003592836, -31.27642233980000697 ) ) ;
#5040=CARTESIAN_POINT ( 'NONE',  ( 0.3828442953759031986, 4.648648069221508194, -35.69999999999999574 ) ) ;
#5047=CARTESIAN_POINT ( 'NONE',  ( -4.338779899226326009, -4.343559731693466652, -10.41399163100000713 ) ) ;
#5048=CARTESIAN_POINT ( 'NONE',  ( 4.634019325638262465, 0.4639887426745106791, -29.63116556699998938 ) ) ;
#5054=CARTESIAN_POINT ( 'NONE',  ( -4.278952157217901231, -0.8066629416743145153, -16.09949426530000238 ) ) ;
#5083=CARTESIAN_POINT ( 'NONE',  ( 1.002713911322309359, 3.977955482547946620, -16.55080441499999466 ) ) ;
#5108=CARTESIAN_POINT ( 'NONE',  ( -5.902313038799129608, -1.548398769286710053, -25.04656121680000425 ) ) ;
#5124=CARTESIAN_POINT ( 'NONE',  ( 3.041701536937339689, -2.824850560391100718, -0.6999999999999994005 ) ) ;
#5139=ORIENTED_EDGE ( 'NONE', *, *, #27706, .F. ) ;
#5149=CARTESIAN_POINT ( 'NONE',  ( 3.486358836775539594, -2.566383416802844319, -8.972776792899997744 ) ) ;
#5155=CARTESIAN_POINT ( 'NONE',  ( -0.7560282158644084927, 4.289996408053712962, -19.83583244400000112 ) ) ;
#5170=CARTESIAN_POINT ( 'NONE',  ( -4.274658871253798509, -0.8336587121505270037, -31.09652066320001040 ) ) ;
#5186=CARTESIAN_POINT ( 'NONE',  ( 0.4316393286370151516, 4.665185289904927757, -35.69999999999999574 ) ) ;
#5193=CARTESIAN_POINT ( 'NONE',  ( 4.262818619062177738, -0.7545854518158021662, -8.771482634699998115 ) ) ;
#5194=CARTESIAN_POINT ( 'NONE',  ( -3.878879136156893281, -1.961445906012333706, -27.96472909260000606 ) ) ;
#5201=CARTESIAN_POINT ( 'NONE',  ( 1.002713911322304696, 3.977955482547951505, -17.05080441500000177 ) ) ;
#5238=CARTESIAN_POINT ( 'NONE',  ( 0.5300456733980246637, -4.293941145674104121, -18.37054674910000429 ) ) ;
#5267=CARTESIAN_POINT ( 'NONE',  ( 1.566980368899947962, 4.067530462867743779, -26.09462237480000724 ) ) ;
#5291=CARTESIAN_POINT ( 'NONE',  ( 3.532024942903766007, -2.488032516543696282, -0.6999999999999994005 ) ) ;
#5315=CARTESIAN_POINT ( 'NONE',  ( 3.834994720502944876, -2.823021758520125601, -8.035276792900001297 ) ) ;
#5320=CARTESIAN_POINT ( 'NONE',  ( -4.219802143832970920, -3.088637908568292012, -19.87254627010000263 ) ) ;
#5333=CARTESIAN_POINT ( 'NONE',  ( -5.984522419796141079, -1.167122196978044535, -31.69652066320000117 ) ) ;
#5351=CARTESIAN_POINT ( 'NONE',  ( 0.5877407897813130555, -4.297347728519515186, -0.3731240480000022619 ) ) ;
#5354=CARTESIAN_POINT ( 'NONE',  ( -3.950034095761360664, 2.484763540022561834, -10.94547590279999838 ) ) ;
#5355=CARTESIAN_POINT ( 'NONE',  ( -2.923929784071483073, -5.123485640109426420, -29.67642233980000910 ) ) ;
#5379=ORIENTED_EDGE ( 'NONE', *, *, #8530, .F. ) ;
#5390=DIRECTION ( 'NONE',  ( -0.8329895880221871440, 0.5532886644841251700, 0.000000000000000000 ) ) ;
#5391=CARTESIAN_POINT ( 'NONE',  ( -3.665401116828205463, 4.874126016103034864, -19.03064294429999848 ) ) ;
#5417=CARTESIAN_POINT ( 'NONE',  ( -1.458225024262878255, -5.692467481908745519, -28.54882611460000419 ) ) ;
#5436=CARTESIAN_POINT ( 'NONE',  ( 3.452488641071199460, -2.537741030969793865, -0.6999999999999991784 ) ) ;
#5468=CARTESIAN_POINT ( 'NONE',  ( -1.782928038406566884, 3.983823234458335527, -23.23780126170000671 ) ) ;
#5483=CARTESIAN_POINT ( 'NONE',  ( -3.866422574246632937, 4.445403037619903408, -29.58728588870000209 ) ) ;
#5500=CARTESIAN_POINT ( 'NONE',  ( -5.017113268509455715, -1.250814956824373159, -0.6999999999999992895 ) ) ;
#5504=CARTESIAN_POINT ( 'NONE',  ( -6.108812354267502798, 0.1812703649498176306, -13.78304957890000360 ) ) ;
#5505=CARTESIAN_POINT ( 'NONE',  ( 4.420334067734101424, -4.199682076162645217, -30.05126389020000488 ) ) ;
#5512=CARTESIAN_POINT ( 'NONE',  ( 4.266075142677475007, -0.9221078188639888484, -23.79036215650000230 ) ) ;
#5541=CARTESIAN_POINT ( 'NONE',  ( -4.448701673712585070, 0.6187532242676665462, -19.25159460730001371 ) ) ;
#5587=CARTESIAN_POINT ( 'NONE',  ( 3.355053135122043173, -2.604011111845283111, -0.6999999999999992895 ) ) ;
#5622=CARTESIAN_POINT ( 'NONE',  ( 0.2540922009626206957, 4.794324758835501576, -23.88168644580000688 ) ) ;
#5637=PRODUCT_DEFINITION_SHAPE ( 'NONE', 'NONE',  #4619 ) ;
#5638=CARTESIAN_POINT ( 'NONE',  ( 2.831388952324535691, -5.386915550550475551, -33.80721934060000677 ) ) ;
#5651=CARTESIAN_POINT ( 'NONE',  ( 2.434861079626372327, 4.402890713382674015, -35.69999999999999574 ) ) ;
#5655=CARTESIAN_POINT ( 'NONE',  ( -3.926812182872200907, 0.9533004182003812499, -0.6999999999999992895 ) ) ;
#5656=CARTESIAN_POINT ( 'NONE',  ( 4.373195337096347224, -2.904765488536225515, 0.6412452698000004059 ) ) ;
#5660=CARTESIAN_POINT ( 'NONE',  ( 4.741512700999319208, 1.965332957690412385, -12.43011350020000272 ) ) ;
#5661=CARTESIAN_POINT ( 'NONE',  ( -2.308365619037855421, -4.044857084274065429, -30.67642233980000199 ) ) ;
#5694=CARTESIAN_POINT ( 'NONE',  ( 4.080592064681261455, -5.083854565965863159, -3.705321867100007438 ) ) ;
#5695=CARTESIAN_POINT ( 'NONE',  ( 4.979326355943800131, -2.377326608238005790, -19.88180150030000348 ) ) ;
#5709=CARTESIAN_POINT ( 'NONE',  ( 4.880902371519058036, -3.592936783560450653, -8.972776792900004850 ) ) ;
#5754=SURFACE_STYLE_USAGE ( .BOTH. , #29677 ) ;
#5776=CARTESIAN_POINT ( 'NONE',  ( 3.805567437367120665, -2.527735466695482991, -0.7070437319000487664 ) ) ;
#5778=CARTESIAN_POINT ( 'NONE',  ( 4.081868536579633222, 3.119100555900671257, -24.30477430109999659 ) ) ;
#5794=CARTESIAN_POINT ( 'NONE',  ( 4.417684705200791484, 4.247747620870205409, -35.32341724620000178 ) ) ;
#5807=CARTESIAN_POINT ( 'NONE',  ( 4.455580650938469667, 2.746354562282469214, -35.69999999999999574 ) ) ;
#5810=CARTESIAN_POINT ( 'NONE',  ( -4.772771908274402008, 1.289969644746177035, -0.6999999999999992895 ) ) ;
#5811=CARTESIAN_POINT ( 'NONE',  ( 2.445722248254770026, -3.773326582131152573, 0.7715606116999971231 ) ) ;
#5815=CARTESIAN_POINT ( 'NONE',  ( -0.6370991518874352666, 4.292107257743940529, -10.86772091660000150 ) ) ;
#5816=CARTESIAN_POINT ( 'NONE',  ( -5.864216825196034932, 1.669623860970033347, -31.30158078969999380 ) ) ;
#5821=CARTESIAN_POINT ( 'NONE',  ( -3.253989917302559043, -2.899813084402115049, -24.84101932450000305 ) ) ;
#5824=ORIENTED_EDGE ( 'NONE', *, *, #27706, .T. ) ;
#5847=CARTESIAN_POINT ( 'NONE',  ( 6.105340317846409626, -0.2107885887935728730, -2.685409721200002320 ) ) ;
#5848=CARTESIAN_POINT ( 'NONE',  ( 3.244870203142138809, 3.966006825147196047, -19.31872222229999991 ) ) ;
#5860=CARTESIAN_POINT ( 'NONE',  ( 1.942707423728255778, -5.758494596869851989, -15.26414732020000464 ) ) ;
#5878=( GEOMETRIC_REPRESENTATION_CONTEXT ( 3 ) GLOBAL_UNCERTAINTY_ASSIGNED_CONTEXT ( ( #22617 ) ) GLOBAL_UNIT_ASSIGNED_CONTEXT ( ( #10311, #3213, #8081 ) ) REPRESENTATION_CONTEXT ( 'NONE', 'WORKASPACE' ) );
#5882=CARTESIAN_POINT ( 'NONE',  ( -5.299969906037439671, -1.662641516789540086, -9.023230888999997035 ) ) ;
#5928=CARTESIAN_POINT ( 'NONE',  ( 3.375516224911109031, -2.766870103071180420, -24.49674734060000247 ) ) ;
#5942=CARTESIAN_POINT ( 'NONE',  ( -3.554763430470064822, 2.566410659217317924, -34.46696136359999940 ) ) ;
#5955=CARTESIAN_POINT ( 'NONE',  ( 1.854139248850241950, 4.609273058799894685, -35.69999999999998153 ) ) ;
#5960=CARTESIAN_POINT ( 'NONE',  ( -4.214204818414113873, 2.192735554227209338, -0.6999999999999992895 ) ) ;
#5961=CARTESIAN_POINT ( 'NONE',  ( -1.949381390262891589, -5.750991590113663676, -0.5756305127000010957 ) ) ;
#5965=CARTESIAN_POINT ( 'NONE',  ( 5.459923716313909381, 2.263110678531865094, -12.49261350019999384 ) ) ;
#5966=CARTESIAN_POINT ( 'NONE',  ( 0.08264113651937701754, -4.780899355463231970, -32.47360030499999795 ) ) ;
#5973=CARTESIAN_POINT ( 'NONE',  ( 3.157381476932438868, -2.999772911539577702, -30.05126389020000488 ) ) ;
#6003=CARTESIAN_POINT ( 'NONE',  ( -1.392415278799817635, -4.107851135794773789, -0.5756305127000010957 ) ) ;
#6004=CARTESIAN_POINT ( 'NONE',  ( -4.219802143827443786, -3.088637908559965339, -17.87254627010000263 ) ) ;
#6021=CARTESIAN_POINT ( 'NONE',  ( 4.080592064764562821, -5.083854566021194010, -3.105321867100004241 ) ) ;
#6040=CARTESIAN_POINT ( 'NONE',  ( 0.3986823046148949556, -5.109930552333694642, -8.455884211800000827 ) ) ;
#6096=CARTESIAN_POINT ( 'NONE',  ( 0.1051796283266584475, -6.084780997910130829, -33.41110030499999795 ) ) ;
#6116=CARTESIAN_POINT ( 'NONE',  ( -3.769085236058943966, 1.982792781023759332, -0.6999999999999992895 ) ) ;
#6117=CARTESIAN_POINT ( 'NONE',  ( 4.080592064681261455, -5.083854565965863159, -3.105321867100004241 ) ) ;
#6121=CARTESIAN_POINT ( 'NONE',  ( 4.945711323160860928, -2.526642934800090945, -12.91474735220000269 ) ) ;
#6122=CARTESIAN_POINT ( 'NONE',  ( 4.198532171036193361, 1.238783022255082189, -35.03159726780000938 ) ) ;
#6140=CARTESIAN_POINT ( 'NONE',  ( 1.353354617599272114, -4.954529841709273796, -0.7000097220332744952 ) ) ;
#6152=CARTESIAN_POINT ( 'NONE',  ( 3.575086008624668299, 1.232431556331196054, -35.69999999999999574 ) ) ;
#6158=CARTESIAN_POINT ( 'NONE',  ( 4.797053106898050423, -0.1656196055093784036, -3.622909721200002764 ) ) ;
#6159=CARTESIAN_POINT ( 'NONE',  ( -1.782928038406565774, 3.983823234458339080, -22.73780126169999605 ) ) ;
#6178=CARTESIAN_POINT ( 'NONE',  ( -3.510061880997908279, 5.032561185093348044, -1.627651354100000169 ) ) ;
#6199=EDGE_CURVE ( 'NONE', #18476, #3989, #19373, .T. ) ;
#6201=CARTESIAN_POINT ( 'NONE',  ( 5.067327387632984959, 4.072231104569050686, -7.754586408000002429 ) ) ;
#6266=CARTESIAN_POINT ( 'NONE',  ( 3.155489075140828437, 3.034105443485042741, -35.32341724620001600 ) ) ;
#6282=CARTESIAN_POINT ( 'NONE',  ( -3.673964118181757943, -4.849481262180703744, -3.128945369300001111 ) ) ;
#6286=CARTESIAN_POINT ( 'NONE',  ( -2.345194346458623347, -4.011532291445385923, -16.18182079289999820 ) ) ;
#6287=CARTESIAN_POINT ( 'NONE',  ( -3.910239773549598397, 2.823051725158805425, -33.52946136360000651 ) ) ;
#6317=CARTESIAN_POINT ( 'NONE',  ( 1.182563860066578654, 3.920765007589456452, -35.70000000000000284 ) ) ;
#6324=CARTESIAN_POINT ( 'NONE',  ( 1.699015317690025118, 6.330513620609809600, -2.053410702900000828 ) ) ;
#6325=CARTESIAN_POINT ( 'NONE',  ( -0.6320852424383932577, 6.069672320066970883, -25.88903409330001182 ) ) ;
#6340=CARTESIAN_POINT ( 'NONE',  ( 0.7420639427752478978, -6.011517603930927045, -18.37054674910000429 ) ) ;
#6363=CARTESIAN_POINT ( 'NONE',  ( -4.799781135534763266, 0.1424267153701331001, -12.24554957890000040 ) ) ;
#6409=DIRECTION ( 'NONE',  ( 0.000000000000000000, 0.000000000000000000, -1.000000000000000000 ) ) ;
#6434=CARTESIAN_POINT ( 'NONE',  ( -5.440024667461782037, 2.837840394948672351, -0.8187643563000029934 ) ) ;
#6438=CARTESIAN_POINT ( 'NONE',  ( 4.630235822890138131, 0.3309221515414816350, -15.14454535870000917 ) ) ;
#6439=CARTESIAN_POINT ( 'NONE',  ( 3.155489075140835542, 3.034105443485036968, -34.82341724620000889 ) ) ;
#6475=CARTESIAN_POINT ( 'NONE',  ( 2.773795135624238295, 4.340636736956414943, -6.138467428499996714 ) ) ;
#6476=CARTESIAN_POINT ( 'NONE',  ( 0.1206012444329082195, -5.909053133798479962, -23.41888333260001431 ) ) ;
#6492=CARTESIAN_POINT ( 'NONE',  ( -5.430430790592723156, -2.746024268427175841, -27.96472909260000606 ) ) ;
#6517=CARTESIAN_POINT ( 'NONE',  ( -2.929853409778804263, 3.622264489389750874, -13.60352819869999763 ) ) ;
#6589=CARTESIAN_POINT ( 'NONE',  ( 1.699015317690025118, 6.330513620609809600, -2.053410702900000828 ) ) ;
#6594=CARTESIAN_POINT ( 'NONE',  ( 3.904356169178446745, -3.871725997715349532, -16.06112212870000633 ) ) ;
#6595=CARTESIAN_POINT ( 'NONE',  ( -5.496316421720869982, 0.7952554554161578304, -33.25783976330001224 ) ) ;
#6629=CARTESIAN_POINT ( 'NONE',  ( 5.506451109007332256, 0.7220432749125509364, -6.626979598400000171 ) ) ;
#6630=CARTESIAN_POINT ( 'NONE',  ( 4.725722714813314518, -3.873618144263061946, -23.99674734060000603 ) ) ;
#6646=CARTESIAN_POINT ( 'NONE',  ( 5.972505199797514486, -1.290950946386169917, -23.79036215650000230 ) ) ;
#6667=CARTESIAN_POINT ( 'NONE',  ( 1.086829820489895848, 5.988658659452708477, -13.42400681849999877 ) ) ;
#6743=CARTESIAN_POINT ( 'NONE',  ( 3.194067125856711264, 4.998308969841025906, -4.200967428500002931 ) ) ;
#6749=CARTESIAN_POINT ( 'NONE',  ( 3.390625094264292372, -3.362288366427768072, -15.99862212869999922 ) ) ;
#6750=CARTESIAN_POINT ( 'NONE',  ( -0.3280975466111886174, 4.681158999438242319, -34.39518930510001127 ) ) ;
#6783=CARTESIAN_POINT ( 'NONE',  ( 1.789657965652164728, 3.567538649943624129, -35.69999999999999574 ) ) ;
#6789=CARTESIAN_POINT ( 'NONE',  ( 4.347198243976404974, 0.5700341643805826308, -5.626979598400000171 ) ) ;
#6790=CARTESIAN_POINT ( 'NONE',  ( -0.4966384047618531139, 4.769028251466922441, -24.95153409330000116 ) ) ;
#6807=CARTESIAN_POINT ( 'NONE',  ( 0.1332961122732720383, -6.531058726825651028, -24.41888333260000365 ) ) ;
#6817=PRODUCT_DEFINITION_FORMATION_WITH_SPECIFIED_SOURCE ( 'ANY', '', #24741, .NOT_KNOWN. ) ;
#6823=CARTESIAN_POINT ( 'NONE',  ( 3.599369630949024845, -3.224860595692283116, -0.6998634107611361177 ) ) ;
#6826=CARTESIAN_POINT ( 'NONE',  ( 3.082386449366550707, -3.056625787687244689, -14.56112212870000810 ) ) ;
#6892=CARTESIAN_POINT ( 'NONE',  ( -1.831588579526983063, 3.958388136463033558, -7.231725184300001885 ) ) ;
#6898=CARTESIAN_POINT ( 'NONE',  ( -2.402234890526806499, 4.289919416549723863, -17.61511783619999960 ) ) ;
#6932=CARTESIAN_POINT ( 'NONE',  ( 0.1986510695968027040, 4.503440677479858323, -35.69999999999999574 ) ) ;
#6943=CARTESIAN_POINT ( 'NONE',  ( -6.505526340832360255, -0.4164809035307331930, -4.748838774899996729 ) ) ;
#6944=CARTESIAN_POINT ( 'NONE',  ( 6.487627055914963137, 0.6495842397260740420, -29.03116556699999862 ) ) ;
#6950=CARTESIAN_POINT ( 'NONE',  ( -0.7873752056533345201, -4.273814420472608511, -3.525234013000005717 ) ) ;
#6962=CARTESIAN_POINT ( 'NONE',  ( -6.074876045044606876, 0.8789665559579967757, -34.25783976329999092 ) ) ;
#6983=CARTESIAN_POINT ( 'NONE',  ( 3.556182480049746353, -3.295754068138798676, -0.6998097270557633864 ) ) ;
#6988=CARTESIAN_POINT ( 'NONE',  ( -4.363437395929424589, 0.1294788321584636748, -12.68304957890000217 ) ) ;
#7056=CARTESIAN_POINT ( 'NONE',  ( 5.214500487626152037, -1.910846663805727541, -4.836105321700002513 ) ) ;
#7061=CARTESIAN_POINT ( 'NONE',  ( 3.244870203142138809, 3.966006825147196047, -21.19372222230000347 ) ) ;
#7093=CARTESIAN_POINT ( 'NONE',  ( 0.7856409681604972217, 4.723271593470196095, -35.69999999999999574 ) ) ;
#7101=CARTESIAN_POINT ( 'NONE',  ( -5.111484982110231279, -0.3272349956394805526, -5.086338774899995308 ) ) ;
#7102=CARTESIAN_POINT ( 'NONE',  ( 3.430850994441077439, -5.010772104901466406, -26.53292313650000622 ) ) ;
#7108=CARTESIAN_POINT ( 'NONE',  ( -1.295942751353772238, 4.166547562507297187, -4.774955258300003891 ) ) ;
#7115=CARTESIAN_POINT ( 'NONE',  ( -6.202057249109299342, 1.908294659314309305, -22.32289663399999924 ) ) ;
#7139=CARTESIAN_POINT ( 'NONE',  ( 3.292208284841127597, -3.106818514002832821, -17.09815260999999964 ) ) ;
#7166=CARTESIAN_POINT ( 'NONE',  ( -4.217400109093717653, 2.917745507991296616, -26.40529765530000361 ) ) ;
#7213=CARTESIAN_POINT ( 'NONE',  ( -5.680091681631305178, 1.608645723366325164, -6.310827254900001293 ) ) ;
#7218=CARTESIAN_POINT ( 'NONE',  ( 3.292208284841127597, -3.106818514002832821, -18.97315261000000319 ) ) ;
#7249=CARTESIAN_POINT ( 'NONE',  ( 0.3471370043377995929, 4.633915050096243604, -35.69999999999999574 ) ) ;
#7259=CARTESIAN_POINT ( 'NONE',  ( -3.099128499470596765, -3.102542665468459138, -10.31399163100000216 ) ) ;
#7260=CARTESIAN_POINT ( 'NONE',  ( 3.790912472548402246, -2.108217834232220866, -26.43037294500000556 ) ) ;
#7266=CARTESIAN_POINT ( 'NONE',  ( -3.331422745097512017, -2.438398348906446689, -18.87254627010000263 ) ) ;
#7294=CARTESIAN_POINT ( 'NONE',  ( 2.911762171867607663, -4.051295066173226544, -0.6999994862911463889 ) ) ;
#7297=CARTESIAN_POINT ( 'NONE',  ( -2.183849900456024784, 3.899926742306370819, -16.17761783619999960 ) ) ;
#7324=CARTESIAN_POINT ( 'NONE',  ( -4.856400125594941386, 3.359828160699422472, -26.46779765530000361 ) ) ;
#7367=CARTESIAN_POINT ( 'NONE',  ( 6.086077541567210147, 0.7980478301550381071, -5.626979598400000171 ) ) ;
#7372=CARTESIAN_POINT ( 'NONE',  ( -3.331422745097512017, -2.438398348906446689, -18.87254627010000263 ) ) ;
#7384=CARTESIAN_POINT ( 'NONE',  ( -4.188726303739424672, 1.192588472141205891, -31.80158078969999735 ) ) ;
#7399=CARTESIAN_POINT ( 'NONE',  ( 0.3593491040380148438, 4.319799995452766161, -35.70000000000000284 ) ) ;
#7406=CARTESIAN_POINT ( 'NONE',  ( 5.967946066639521874, -1.056419632483374116, -9.371482634700001313 ) ) ;
#7407=CARTESIAN_POINT ( 'NONE',  ( -4.346598770676711965, -0.007247149673127636568, -27.66856466010000659 ) ) ;
#7414=CARTESIAN_POINT ( 'NONE',  ( 4.347198243976404974, 0.5700341643805826308, -5.626979598400000171 ) ) ;
#7447=CARTESIAN_POINT ( 'NONE',  ( 1.102985302404366097, 4.375751030832064181, -16.11330441500000177 ) ) ;
#7471=CARTESIAN_POINT ( 'NONE',  ( 0.09521150875770739708, -4.665041947735808492, -24.41888333260000365 ) ) ;
#7517=CARTESIAN_POINT ( 'NONE',  ( 0.5074138422395748638, -6.503547975687064664, -9.393384211799999051 ) ) ;
#7523=CARTESIAN_POINT ( 'NONE',  ( -1.058439502263211374, 6.005994971325610443, -20.43583244400000609 ) ) ;
#7539=CARTESIAN_POINT ( 'NONE',  ( -5.414567903583902719, -1.055967702048432599, -32.09652066320001751 ) ) ;
#7554=CARTESIAN_POINT ( 'NONE',  ( 0.3780721272196958527, 4.308878343199122440, -35.69999999999999574 ) ) ;
#7556=CARTESIAN_POINT ( 'NONE',  ( -3.751900487315417809, -0.8603159972124789778, -0.6999999999999994005 ) ) ;
#7560=CARTESIAN_POINT ( 'NONE',  ( 0.2164205762250857590, 5.520452575866341860, -8.937690181099998910 ) ) ;
#7561=CARTESIAN_POINT ( 'NONE',  ( 2.193772516446764076, 5.694542648089183423, -25.49462237480000582 ) ) ;
#7566=CARTESIAN_POINT ( 'NONE',  ( -4.180754675048095947, 1.217138862148074763, -16.30443125759999745 ) ) ;
#7598=CARTESIAN_POINT ( 'NONE',  ( -2.402234890526806499, 4.289919416549723863, -15.74011783620000671 ) ) ;
#7621=CARTESIAN_POINT ( 'NONE',  ( -5.367600138796280618, 3.713494282865395402, -26.06779765530001214 ) ) ;
#7639=CARTESIAN_POINT ( 'NONE',  ( 3.205646567073016318, -2.709343606966754248, -0.6999999999999992895 ) ) ;
#7662=CARTESIAN_POINT ( 'NONE',  ( 3.981471518793421538, 3.199610153647690414, -7.417086408000004738 ) ) ;
#7667=CARTESIAN_POINT ( 'NONE',  ( -2.227024806490486508, -3.476280271252723431, -18.70544088819999118 ) ) ;
#7681=CARTESIAN_POINT ( 'NONE',  ( 1.456545767631115096, -4.104408573385633474, -30.75632401680000072 ) ) ;
#7702=CARTESIAN_POINT ( 'NONE',  ( -2.240416623506871208, -3.018983424413556715, -0.6999999999999992895 ) ) ;
#7703=FACE_OUTER_BOUND ( 'NONE', #25157, .T. ) ;
#7705=CARTESIAN_POINT ( 'NONE',  ( -4.602605444716575178, -1.443872896163948205, -10.96073088899999526 ) ) ;
#7706=CARTESIAN_POINT ( 'NONE',  ( -3.231711866632715147, -5.662799918003592836, -30.67642233980000199 ) ) ;
#7745=CARTESIAN_POINT ( 'NONE',  ( -3.057389860650357338, 5.459897439232808125, -16.67761783620000315 ) ) ;
#7774=CARTESIAN_POINT ( 'NONE',  ( -0.6320852424383932577, 6.069672320066970883, -26.48903409330001679 ) ) ;
#7793=CARTESIAN_POINT ( 'NONE',  ( 2.392384901021629151, -3.229711410377742453, -0.6999999999999992895 ) ) ;
#7820=CARTESIAN_POINT ( 'NONE',  ( -5.857861475075242019, -1.837656413297739766, -10.02323088899999881 ) ) ;
#7825=CARTESIAN_POINT ( 'NONE',  ( 5.972505199797514486, -1.290950946386169917, -24.39036215650000727 ) ) ;
#7836=CARTESIAN_POINT ( 'NONE',  ( 0.7775660777938816492, 5.461502024334397909, -30.00600711720000291 ) ) ;
#7853=CARTESIAN_POINT ( 'NONE',  ( -3.832152770726432678, 2.440039442800121083, -0.6999999999999992895 ) ) ;
#7854=CARTESIAN_POINT ( 'NONE',  ( -1.392415278799817635, -4.107851135794773789, -0.5756305127000010957 ) ) ;
#7856=CARTESIAN_POINT ( 'NONE',  ( 1.348918213770420316, 4.124136235849971577, -11.57047964829999742 ) ) ;
#7857=CARTESIAN_POINT ( 'NONE',  ( 3.473119624653126181, -3.299750202710006963, -29.11376389020000133 ) ) ;
#7865=CARTESIAN_POINT ( 'NONE',  ( -1.782928038406565774, 3.983823234458339080, -22.73780126169999605 ) ) ;
#7896=CARTESIAN_POINT ( 'NONE',  ( -4.873044981369978323, 1.499374375125315684, -21.38539663400000634 ) ) ;
#7914=VERTEX_POINT ( 'NONE', #25989 ) ;
#7943=CARTESIAN_POINT ( 'NONE',  ( 3.043036374812654099, -2.823920995556914004, -0.6999999999999992895 ) ) ;
#7953=PRESENTATION_STYLE_ASSIGNMENT (( #5754 ) ) ;
#7976=CARTESIAN_POINT ( 'NONE',  ( -4.430040892179064826, 1.363067613765865937, -22.82289663400000279 ) ) ;
#7989=EDGE_CURVE ( 'NONE', #18476, #21685, #8615, .T. ) ;
#7992=CARTESIAN_POINT ( 'NONE',  ( -4.346598770676711965, -0.007247149673127636568, -28.66856466010000304 ) ) ;
#8009=CARTESIAN_POINT ( 'NONE',  ( -3.983623483853893088, 2.386763808281609389, -0.6999999999999992895 ) ) ;
#8013=CARTESIAN_POINT ( 'NONE',  ( 6.034652528523337445, 2.501332855249893683, -11.49261350020000449 ) ) ;
#8014=CARTESIAN_POINT ( 'NONE',  ( 3.157381476932438868, -2.999772911539577702, -30.05126389020000488 ) ) ;
#8021=CARTESIAN_POINT ( 'NONE',  ( 2.450607853129164848, -3.579122932049590755, -27.13292313650000764 ) ) ;
#8050=CARTESIAN_POINT ( 'NONE',  ( 5.003468744149685676, 2.348385630676867564, -3.479170051700001043 ) ) ;
#8051=CARTESIAN_POINT ( 'NONE',  ( 5.516020573121914516, 0.1374401492888292498, -19.67661200060000226 ) ) ;
#8064=CARTESIAN_POINT ( 'NONE',  ( 4.190083271651539043, -3.954132654223795562, -18.03565260999999964 ) ) ;
#8081=( NAMED_UNIT ( * ) SI_UNIT ( $, .STERADIAN. ) SOLID_ANGLE_UNIT ( ) );
#8094=CARTESIAN_POINT ( 'NONE',  ( 0.6576816962115121790, -3.783751283609423144, -0.6999999999999992895 ) ) ;
#8123=CARTESIAN_POINT ( 'NONE',  ( 0.3233900739386466605, 6.101867874933233793, -23.54418644580000120 ) ) ;
#8139=CARTESIAN_POINT ( 'NONE',  ( -0.3280975466111932248, 4.681158999438244983, -34.89518930510001127 ) ) ;
#8155=CARTESIAN_POINT ( 'NONE',  ( -3.942867718245478770, 0.7271718878511516104, -0.6999999999999992895 ) ) ;
#8160=CARTESIAN_POINT ( 'NONE',  ( 3.665953941183818010, 4.858601989977915814, -14.22796858840000311 ) ) ;
#8161=CARTESIAN_POINT ( 'NONE',  ( 1.456545767631115096, -4.104408573385633474, -29.75632401680000427 ) ) ;
#8166=CARTESIAN_POINT ( 'NONE',  ( 1.882647771056455976, 3.960165260869605408, -32.15113063600000487 ) ) ;
#8197=CARTESIAN_POINT ( 'NONE',  ( 3.123710955063065509, -2.074832491810036039, -0.4587547302000010707 ) ) ;
#8198=CARTESIAN_POINT ( 'NONE',  ( -2.942059828035410440, -4.605008556695580957, -20.70891267849999906 ) ) ;
#8211=CARTESIAN_POINT ( 'NONE',  ( 1.699015317690025118, 6.330513620609809600, -2.053410702900000828 ) ) ;
#8247=CARTESIAN_POINT ( 'NONE',  ( -0.1094138230076618645, -3.801899662088418008, -0.6999999999999994005 ) ) ;
#8282=CARTESIAN_POINT ( 'NONE',  ( 4.725722714813314518, -3.873618144263061946, -23.99674734060000603 ) ) ;
#8295=CARTESIAN_POINT ( 'NONE',  ( -4.773116892509256637, 0.6906165796890335606, -35.19533976329999803 ) ) ;
#8312=CARTESIAN_POINT ( 'NONE',  ( -3.748827661146469481, 2.120144271060945051, -0.6999999999999992895 ) ) ;
#8313=CARTESIAN_POINT ( 'NONE',  ( 5.530149664617865390, 2.595584118083901881, -2.479170051700001043 ) ) ;
#8316=CARTESIAN_POINT ( 'NONE',  ( -0.7008090670319790938, 4.721317983490957992, -11.80522091660000505 ) ) ;
#8317=CARTESIAN_POINT ( 'NONE',  ( 2.831388952324535691, -5.386915550550475551, -33.20721934060000535 ) ) ;
#8352=CARTESIAN_POINT ( 'NONE',  ( 6.105340317846409626, -0.2107885887935728730, -3.285409721200005517 ) ) ;
#8353=CARTESIAN_POINT ( 'NONE',  ( -3.251750336246070461, -5.089746299513510763, -21.70891267860000795 ) ) ;
#8368=CARTESIAN_POINT ( 'NONE',  ( 3.665953941183818010, 4.858601989977915814, -14.22796858840000311 ) ) ;
#8389=CARTESIAN_POINT ( 'NONE',  ( 4.584724779323398280, 3.684399570781342614, -7.354586408000001185 ) ) ;
#8451=CARTESIAN_POINT ( 'NONE',  ( -4.901082056047598279, -4.330235462250267453, -34.43447003409999496 ) ) ;
#8468=CARTESIAN_POINT ( 'NONE',  ( -4.062788589238770953, 2.328859124429163430, -0.6999999999999992895 ) ) ;
#8469=CARTESIAN_POINT ( 'NONE',  ( 3.950106903291103588, 1.853988655799144958, -2.479170051700008148 ) ) ;
#8474=CARTESIAN_POINT ( 'NONE',  ( -4.101794773660127902, 5.071170285176791914, -14.20352819870000083 ) ) ;
#8475=CARTESIAN_POINT ( 'NONE',  ( 3.471037982653067733, 3.337515987827158526, -34.38591724620000178 ) ) ;
#8509=CARTESIAN_POINT ( 'NONE',  ( 2.223383862040879677, -3.430296892840221101, -0.6659393883000006564 ) ) ;
#8510=CARTESIAN_POINT ( 'NONE',  ( -3.251750336246070461, -5.089746299513510763, -21.10891267850000119 ) ) ;
#8528=CARTESIAN_POINT ( 'NONE',  ( 5.530149664617865390, 2.595584118083901881, -2.479170051700001043 ) ) ;
#8530=EDGE_CURVE ( 'NONE', #23432, #27907, #26953, .T. ) ;
#8551=CARTESIAN_POINT ( 'NONE',  ( 5.399570250832249840, -0.9558082389699539272, -7.771482634700006109 ) ) ;
#8572=FILL_AREA_STYLE ('',( #12993 ) ) ;
#8608=CARTESIAN_POINT ( 'NONE',  ( 3.471037982653067733, 3.337515987827158526, -36.26091724619999468 ) ) ;
#8615=B_SPLINE_CURVE_WITH_KNOTS ( 'NONE', 3,
 ( #17147, #7702, #4737, #23949, #11970, #9451, #497, #17304, #7556, #19524, #28651, #21581, #28, #21727, #10852, #8155, #17751, #10542, #17907, #5655, #19977, #27215, #15254, #29881, #797, #1094, #13044, #29573, #10386, #20281, #6116, #27670, #8312, #22502, #647, #3596, #22804, #20137, #24553, #2992, #27514, #12737, #13190, #25007, #7853, #18065, #8009, #29727, #8468, #22651, #10235, #17607, #24863, #5960, #29417, #15107, #19835, #3292, #952, #27370, #30035, #12896, #5810, #15408, #3441, #22346, #10685, #15554, #25164, #17456, #27062, #1255, #12582, #20438, #22190, #5500, #24702, #3138, #11320, #20753, #20918, #1412, #30360 ),
 .UNSPECIFIED., .F., .F.,
 ( 4, 2, 2, 1, 1, 1, 2, 2, 1, 1, 1, 1, 1, 2, 2, 1, 1, 1, 1, 2, 2, 1, 1, 1, 1, 1, 2, 2, 1, 1, 2, 2, 1, 1, 1, 1, 2, 2, 1, 1, 1, 2, 2, 1, 1, 2, 2, 2, 2, 1, 1, 2, 2, 1, 2, 2, 4 ),
 ( 0.000000000000000000, 0.06249999999999655831, 0.1249999999999931166, 0.1874999999999896749, 0.2187499999999879541, 0.2343749999999871214, 0.2421874999999866773, 0.2499999999999862332, 0.3124999999999829026, 0.3437499999999812372, 0.3593749999999803491, 0.3671874999999799605, 0.3710937499999797384, 0.3730468749999796274, 0.3749999999999795164, 0.4062499999999776290, 0.4218749999999767408, 0.4296874999999762967, 0.4335937499999760747, 0.4355468749999759637, 0.4374999999999758526, 0.4531249999999749090, 0.4609374999999744649, 0.4648437499999742428, 0.4667968749999741873, 0.4677734374999740763, 0.4682617187499739653, 0.4687499999999739098, 0.4843749999999711342, 0.4921874999999697464, 0.4960937499999689693, 0.4999999999999681921, 0.5156249999999658051, 0.5234374999999645839, 0.5273437499999639178, 0.5292968749999636957, 0.5302734374999636957, 0.5312499999999636957, 0.5468749999999640288, 0.5546874999999642508, 0.5585937499999643618, 0.5605468749999643618, 0.5624999999999643618, 0.5937499999999672484, 0.6093749999999685807, 0.6171874999999692468, 0.6249999999999699130, 0.6562499999999723554, 0.6874999999999749090, 0.7187499999999773515, 0.7343749999999786837, 0.7421874999999792388, 0.7499999999999797939, 0.8124999999999847899, 0.8437499999999872324, 0.8749999999999897859, 1.000000000000000000 ),
 .UNSPECIFIED. ) ;
#8625=CARTESIAN_POINT ( 'NONE',  ( 2.914708617673698932, -3.631324690002109445, -3.105321867099997135 ) ) ;
#8629=CARTESIAN_POINT ( 'NONE',  ( 1.387648159808044790, -4.113210426322153168, -15.76414732019999931 ) ) ;
#8630=CARTESIAN_POINT ( 'NONE',  ( -4.339197174995631734, 0.6278332542688225271, -34.25783976329999092 ) ) ;
#8665=ADVANCED_FACE ( 'NONE', ( #10277 ), #27791, .T. ) ;
#8670=CARTESIAN_POINT ( 'NONE',  ( 2.914708617673689606, -3.631324690002112110, -3.605321867100001576 ) ) ;
#8671=CARTESIAN_POINT ( 'NONE',  ( 0.2309929099465271585, 4.358477053493584386, -22.94418644579999977 ) ) ;
#8677=CARTESIAN_POINT ( 'NONE',  ( -2.400531359713943491, -2.916784241273735923, -0.7578093795000060418 ) ) ;
#8685=CARTESIAN_POINT ( 'NONE',  ( -6.505526340826822462, -0.4164809035224065203, -4.148838774900000637 ) ) ;
#8711=CARTESIAN_POINT ( 'NONE',  ( 2.789765316938662476, -3.934254546267435426, -11.18638893669999668 ) ) ;
#8773=CARTESIAN_POINT ( 'NONE',  ( 4.373195337096333013, -2.904765488536246387, -35.95875473020000612 ) ) ;
#8789=CARTESIAN_POINT ( 'NONE',  ( -5.111484982110231279, -0.3272349956394805526, -3.211338774900002413 ) ) ;
#8793=CARTESIAN_POINT ( 'NONE',  ( -2.970579505556664834, -5.081274235795743444, -16.68182079290001241 ) ) ;
#8794=CARTESIAN_POINT ( 'NONE',  ( 3.436082050571383828, -2.282315740991611719, -35.02125473019999902 ) ) ;
#8828=CARTESIAN_POINT ( 'NONE',  ( 4.528382002446963206, -1.659419471228278375, -6.773605321699999848 ) ) ;
#8829=CARTESIAN_POINT ( 'NONE',  ( 4.266075142677475007, -0.9221078188639888484, -23.79036215650000230 ) ) ;
#8845=CARTESIAN_POINT ( 'NONE',  ( 6.487627055914963137, 0.6495842397260740420, -29.63116556699998938 ) ) ;
#8868=CARTESIAN_POINT ( 'NONE',  ( -1.499765329346335108, -5.740821375879678001, -11.55022317839999424 ) ) ;
#8895=COLOUR_RGB ( '', 0.09019608, 0.27058824, 0.51372549) ;
#8948=CARTESIAN_POINT ( 'NONE',  ( 5.003468744149685676, 2.348385630676867564, -1.479170051700001487 ) ) ;
#8953=CARTESIAN_POINT ( 'NONE',  ( -2.766209873889304394, 4.939907206908331183, -17.67761783620000671 ) ) ;
#8970=CARTESIAN_POINT ( 'NONE',  ( 1.191496624263074233, -5.005312061620236008, -0.6999976953858815243 ) ) ;
#8990=CARTESIAN_POINT ( 'NONE',  ( -3.673964118181757943, -4.849481262180703744, -4.328945369300001289 ) ) ;
#8991=CARTESIAN_POINT ( 'NONE',  ( 0.2540922009626206957, 4.794324758835501576, -22.00668644580000688 ) ) ;
#9006=CARTESIAN_POINT ( 'NONE',  ( 5.245096043587340162, -0.2338077457563897399, -35.69999999999999574 ) ) ;
#9029=CARTESIAN_POINT ( 'NONE',  ( 2.618538529469167653, 3.470429992801025154, -13.72796858840000489 ) ) ;
#9085=CARTESIAN_POINT ( 'NONE',  ( 5.132309988016721114, -0.8582124304006011339, -36.74517599850001659 ) ) ;
#9100=CARTESIAN_POINT ( 'NONE',  ( -1.814319851916122772, 5.833166587536846137, -4.774955258300003891 ) ) ;
#9105=CARTESIAN_POINT ( 'NONE',  ( 2.326244606069574505, 3.379075471592551949, -17.21259163650000446 ) ) ;
#9114=CARTESIAN_POINT ( 'NONE',  ( 49.56288048729999218, -32.92067553680000458, 44.14124526979999530 ) ) ;
#9132=CARTESIAN_POINT ( 'NONE',  ( 2.004564144564168870, 3.412403539796502461, -35.69999999999999574 ) ) ;
#9139=CARTESIAN_POINT ( 'NONE',  ( -3.052679639724400928, 3.117809041995142749, -4.568732180599999637 ) ) ;
#9140=CARTESIAN_POINT ( 'NONE',  ( -3.834000099192785616, 2.652495916366752304, -24.96779765530000361 ) ) ;
#9156=CARTESIAN_POINT ( 'NONE',  ( 6.096654317653251276, 0.1519075334279890166, -20.67661200060000226 ) ) ;
#9174=CARTESIAN_POINT ( 'NONE',  ( 1.557513348718032375, -4.881019519337725043, -0.7000303665504261641 ) ) ;
#9177=CARTESIAN_POINT ( 'NONE',  ( -5.527020701484460119, 0.1640065206915941320, -12.18304957889999862 ) ) ;
#9251=CARTESIAN_POINT ( 'NONE',  ( 2.246931792404676997, -6.149078805876593279, -6.260585232200001293 ) ) ;
#9256=CARTESIAN_POINT ( 'NONE',  ( 4.130711734062736618, 1.221343755424965316, -17.54190840230000248 ) ) ;
#9299=CARTESIAN_POINT ( 'NONE',  ( -2.723504195107721237, -4.795398582787750108, -7.685065142700002738 ) ) ;
#9301=CARTESIAN_POINT ( 'NONE',  ( -4.913246905806704312, -2.484498147601009510, -26.96472909260000250 ) ) ;
#9337=CARTESIAN_POINT ( 'NONE',  ( 1.942707423728255778, -5.758494596869851989, -14.66414732020000855 ) ) ;
#9410=CARTESIAN_POINT ( 'NONE',  ( -2.320012200738846619, 5.013958306206127702, -6.731725184299999221 ) ) ;
#9414=CARTESIAN_POINT ( 'NONE',  ( 0.7420639427752478978, -6.011517603930927045, -18.97054674910000927 ) ) ;
#9447=CARTESIAN_POINT ( 'NONE',  ( 0.2496999827216928036, 4.399169623874717772, -35.69999999999998863 ) ) ;
#9451=CARTESIAN_POINT ( 'NONE',  ( -3.305579555868532804, -1.864813555827612879, -0.6999999999999992895 ) ) ;
#9455=CARTESIAN_POINT ( 'NONE',  ( -4.598206294437411579, -3.044638162784917945, -7.889929326000002519 ) ) ;
#9456=CARTESIAN_POINT ( 'NONE',  ( 4.807767551039155762, 1.738376938488521040, -25.57499766020000109 ) ) ;
#9463=CARTESIAN_POINT ( 'NONE',  ( 4.262818619062177738, -0.7545854518158021662, -8.771482634699998115 ) ) ;
#9473=ORIENTED_EDGE ( 'NONE', *, *, #9801, .F. ) ;
#9475=CARTESIAN_POINT ( 'NONE',  ( 4.129834804004070214, 5.047645050185102455, -20.25622222230000347 ) ) ;
#9498=CARTESIAN_POINT ( 'NONE',  ( 5.232234863148874204, 1.547035423556993639, -16.54190840230001669 ) ) ;
#9527=CARTESIAN_POINT ( 'NONE',  ( -4.637531673247329955, -1.216599033067103264, -25.98406121680000425 ) ) ;
#9575=CARTESIAN_POINT ( 'NONE',  ( -1.425537026491585868, 4.583202318768851313, -3.837455258300006555 ) ) ;
#9580=CARTESIAN_POINT ( 'NONE',  ( 1.771049722044198971, -6.234229536879996481, -21.29535708919999593 ) ) ;
#9608=CARTESIAN_POINT ( 'NONE',  ( 0.7946872764172051573, 4.107354228457116285, -35.69999999999999574 ) ) ;
#9614=CARTESIAN_POINT ( 'NONE',  ( -4.184186767956290964, -1.312611723764788296, -10.52323088900000414 ) ) ;
#9615=CARTESIAN_POINT ( 'NONE',  ( -5.430430790592723156, -2.746024268427175841, -27.36472909260000108 ) ) ;
#9620=CARTESIAN_POINT ( 'NONE',  ( -3.950034095761355335, 2.484763540022569384, -10.44547590280000371 ) ) ;
#9647=CARTESIAN_POINT ( 'NONE',  ( 2.926699082014111664, -4.037750131915458063, -0.6999994991842533043 ) ) ;
#9651=CARTESIAN_POINT ( 'NONE',  ( 0.5300456733980305479, -4.293941145674102344, -17.87054674910000784 ) ) ;
#9677=CARTESIAN_POINT ( 'NONE',  ( -4.266767049786682087, -2.157590496602210806, -28.90222909260000250 ) ) ;
#9683=AXIS2_PLACEMENT_3D ( 'NONE', #12171, #19730, #12479 ) ;
#9701=B_SPLINE_CURVE_WITH_KNOTS ( 'NONE', 3,
 ( #24332, #585, #20219, #12670, #5291, #22438, #29811, #883, #14734, #5436, #22125, #10166, #22595, #24486, #24945, #5587, #19610, #1035, #17687, #17845, #29665, #7639, #19766, #24639, #14894, #2923, #26841, #7943, #5124, #431, #3072, #22277, #29351, #12516, #7793, #735, #17394, #26997, #10326, #12835, #19920, #10013, #15046, #8094, #29507, #15347, #8247, #17543, #27153, #10478, #10624, #15188, #24792 ),
 .UNSPECIFIED., .F., .F.,
 ( 4, 1, 1, 1, 2, 2, 1, 1, 1, 1, 2, 2, 1, 1, 2, 2, 1, 1, 1, 2, 2, 1, 1, 1, 2, 2, 1, 1, 2, 2, 2, 2, 2, 2, 4 ),
 ( 0.000000000000000000, 0.01562499999999919509, 0.02343749999999868161, 0.02734374999999848038, 0.02929687499999846997, 0.03124999999999845957, 0.04687499999999945877, 0.05468749999999995837, 0.05859375000000026368, 0.06054687500000038858, 0.06152343750000032613, 0.06250000000000026368, 0.07812499999999922284, 0.08593749999999863998, 0.08984374999999845957, 0.09374999999999829303, 0.1093749999999974187, 0.1171874999999970440, 0.1210937499999970163, 0.1230468749999969330, 0.1249999999999968636, 0.1874999999999967248, 0.2187499999999966138, 0.2343749999999964750, 0.2421874999999965306, 0.2499999999999966138, 0.3749999999999971134, 0.4374999999999973355, 0.4687499999999975020, 0.4999999999999976685, 0.5624999999999980016, 0.6249999999999982236, 0.7499999999999987788, 0.8749999999999993339, 1.000000000000000000 ),
 .UNSPECIFIED. ) ;
#9720=MECHANICAL_DESIGN_GEOMETRIC_PRESENTATION_REPRESENTATION('',(#19275),#4203);
#9723=CARTESIAN_POINT ( 'NONE',  ( 5.763395275750641922, -2.111988417859953504, -5.836105321700000736 ) ) ;
#9728=CARTESIAN_POINT ( 'NONE',  ( 4.129834804009608007, 5.047645050193429128, -20.85622222230000489 ) ) ;
#9745=CARTESIAN_POINT ( 'NONE',  ( 1.844957972340690588, -5.198917526286033208, -31.25632401680000783 ) ) ;
#9760=CARTESIAN_POINT ( 'NONE',  ( 0.2104509476007864199, 4.444330529862462242, -35.69999999999998863 ) ) ;
#9771=CARTESIAN_POINT ( 'NONE',  ( 0.2392016894930265591, 6.101552847015987879, -8.537690181100003883 ) ) ;
#9772=CARTESIAN_POINT ( 'NONE',  ( -6.085238278930475531, -0.01014600953121863602, -28.16856466009999593 ) ) ;
#9781=CARTESIAN_POINT ( 'NONE',  ( 4.630235822890134578, 0.3309221515414850767, -14.64454535870000207 ) ) ;
#9801=EDGE_CURVE ( 'NONE', #27907, #3989, #30309, .T. ) ;
#9812=CARTESIAN_POINT ( 'NONE',  ( 5.320018516182488000, -2.211191048809329374, -17.87122516810000405 ) ) ;
#9838=CARTESIAN_POINT ( 'NONE',  ( 3.790912472548403578, -2.108217834232220422, -26.93037294500000201 ) ) ;
#9883=CARTESIAN_POINT ( 'NONE',  ( 0.2392016894930265591, 6.101552847015987879, -7.937690181100006903 ) ) ;
#9888=CARTESIAN_POINT ( 'NONE',  ( -3.316315296248301792, 4.409923538414076027, -20.63064294429999990 ) ) ;
#9904=CARTESIAN_POINT ( 'NONE',  ( 2.499950477468915189, 3.566222500441431187, -29.71106724380000230 ) ) ;
#9921=CARTESIAN_POINT ( 'NONE',  ( 0.3669718430465309100, 4.315306525164807283, -35.70000000000000995 ) ) ;
#9927=CARTESIAN_POINT ( 'NONE',  ( 0.1879441846346346090, 4.794077236920960772, -8.875190181100002462 ) ) ;
#9928=CARTESIAN_POINT ( 'NONE',  ( 5.097421258188004067, 0.5103876169533114737, -28.69366556700000004 ) ) ;
#9935=CARTESIAN_POINT ( 'NONE',  ( 2.992916622598568388, -2.824380467281232487, -18.03565260999999964 ) ) ;
#9968=CARTESIAN_POINT ( 'NONE',  ( -4.598830142556993295, 1.338852748371190282, -15.36693125759999923 ) ) ;
#9993=CARTESIAN_POINT ( 'NONE',  ( -4.121720561938956529, -3.673096573571036139, -25.84101932450001016 ) ) ;
#10013=CARTESIAN_POINT ( 'NONE',  ( 0.9747465533911489066, -3.736773033513550946, -0.6999999999999991784 ) ) ;
#10042=CARTESIAN_POINT ( 'NONE',  ( 5.967946066639521874, -1.056419632483374116, -8.171482634700002023 ) ) ;
#10048=CARTESIAN_POINT ( 'NONE',  ( 4.354753084053725409, 0.1085053810021691101, -20.67661200060000226 ) ) ;
#10062=CARTESIAN_POINT ( 'NONE',  ( 3.473119624653126181, -3.299750202710006963, -30.98876389020000133 ) ) ;
#10076=LINE ( 'NONE', #12115, #15269 ) ;
#10078=CARTESIAN_POINT ( 'NONE',  ( 0.4552590567128736998, 4.266916551624608367, -35.70000000000000284 ) ) ;
#10083=CARTESIAN_POINT ( 'NONE',  ( 2.223383862040885450, -3.430296892840217993, -0.1659393883000001568 ) ) ;
#10086=CARTESIAN_POINT ( 'NONE',  ( 3.619519562537647062, 2.908736503316577515, -8.854586407999997633 ) ) ;
#10087=CARTESIAN_POINT ( 'NONE',  ( -4.607598934103576127, 1.311847319348407481, -30.36408078970000801 ) ) ;
#10093=CARTESIAN_POINT ( 'NONE',  ( -1.932773295258156887, 4.259541830411037289, -31.72635571290000200 ) ) ;
#10123=CARTESIAN_POINT ( 'NONE',  ( -3.117834729128555971, -4.866792379758847709, -18.10544088820000042 ) ) ;
#10150=CARTESIAN_POINT ( 'NONE',  ( -3.253989917302559043, -2.899813084402115049, -24.84101932450000305 ) ) ;
#10166=CARTESIAN_POINT ( 'NONE',  ( 3.380431529615641750, -2.586477721823119857, -0.6999999999999992895 ) ) ;
#10195=CARTESIAN_POINT ( 'NONE',  ( -3.099128499470596321, -3.102542665468454253, -9.813991631000003935 ) ) ;
#10197=ORIENTED_EDGE ( 'NONE', *, *, #1046, .F. ) ;
#10201=CARTESIAN_POINT ( 'NONE',  ( 0.1332961122732720383, -6.531058726825651028, -25.01888333259999442 ) ) ;
#10214=CARTESIAN_POINT ( 'NONE',  ( -5.864216825201565619, 1.669623860961706674, -31.90158078969999877 ) ) ;
#10235=CARTESIAN_POINT ( 'NONE',  ( -4.082901699294640530, 2.312515566788601262, -0.6999999999999991784 ) ) ;
#10238=CARTESIAN_POINT ( 'NONE',  ( 4.880902371519058036, -3.592936783560450653, -9.572776792900008047 ) ) ;
#10239=CARTESIAN_POINT ( 'NONE',  ( 2.022420680230021972, -3.847796821814266632, -33.20721934060000535 ) ) ;
#10245=CARTESIAN_POINT ( 'NONE',  ( 0.09521150875770739708, -4.665041947735808492, -24.41888333260000365 ) ) ;
#10277=FACE_OUTER_BOUND ( 'NONE', #20005, .T. ) ;
#10278=CARTESIAN_POINT ( 'NONE',  ( 3.736517203680826515, 4.566916950137848374, -19.25622222229999991 ) ) ;
#10311=( LENGTH_UNIT ( ) NAMED_UNIT ( * ) SI_UNIT ( .MILLI., .METRE. ) );
#10326=CARTESIAN_POINT ( 'NONE',  ( 1.343267674844191406, -3.656436453084884519, -0.6999999999999991784 ) ) ;
#10357=CARTESIAN_POINT ( 'NONE',  ( -4.873044981369978323, 1.499374375125315684, -23.26039663399999924 ) ) ;
#10371=CARTESIAN_POINT ( 'NONE',  ( -2.126050624815288614, 4.685496013473724020, -32.66385571289999490 ) ) ;
#10384=CARTESIAN_POINT ( 'NONE',  ( 3.114464126964767932, 4.033014307823163946, -35.69999999999999574 ) ) ;
#10386=CARTESIAN_POINT ( 'NONE',  ( -3.808450222011727782, 1.763428524318019219, -0.6999999999999992895 ) ) ;
#10391=CARTESIAN_POINT ( 'NONE',  ( 0.7763070146520680836, 4.277613328189620923, -14.02400681850000197 ) ) ;
#10392=CARTESIAN_POINT ( 'NONE',  ( 2.635706879431563898, 5.544231365240147369, -31.55113063599999990 ) ) ;
#10429=CARTESIAN_POINT ( 'NONE',  ( 3.950106903291103588, 1.853988655799144958, -2.479170051700008148 ) ) ;
#10430=CARTESIAN_POINT ( 'NONE',  ( 4.129834804009608007, 5.047645050193429128, -20.25622222230000347 ) ) ;
#10444=CARTESIAN_POINT ( 'NONE',  ( -3.117834729128555971, -4.866792379758847709, -18.70544088820000184 ) ) ;
#10478=CARTESIAN_POINT ( 'NONE',  ( -1.111489881331200413, -3.601265787235460536, -0.6999999999999994005 ) ) ;
#10510=CARTESIAN_POINT ( 'NONE',  ( -2.496099253731141943, 5.577352528212363048, -23.33780126170000102 ) ) ;
#10525=CARTESIAN_POINT ( 'NONE',  ( -4.976668802704899086, 3.592974922927941073, -35.06696136360000793 ) ) ;
#10537=CARTESIAN_POINT ( 'NONE',  ( 3.944225552621728692, 3.331202856656692468, -35.69999999999999574 ) ) ;
#10542=CARTESIAN_POINT ( 'NONE',  ( -3.930544418528015616, 0.9096215242735280482, -0.6999999999999994005 ) ) ;
#10546=CARTESIAN_POINT ( 'NONE',  ( -2.929853409778804263, 3.622264489389750874, -13.60352819869999763 ) ) ;
#10547=CARTESIAN_POINT ( 'NONE',  ( 3.503437880484509659, 2.636891074944046398, -32.36032172559999509 ) ) ;
#10581=CARTESIAN_POINT ( 'NONE',  ( 1.699015317690025118, 6.330513620609809600, -2.653410702900004026 ) ) ;
#10582=CARTESIAN_POINT ( 'NONE',  ( 1.602378319964792297, -5.640493390528545703, -20.29535708920000658 ) ) ;
#10595=CARTESIAN_POINT ( 'NONE',  ( -4.262638389374871828, -3.164596713843205400, -0.8737437981000060194 ) ) ;
#10624=CARTESIAN_POINT ( 'NONE',  ( -1.580768150575516229, -3.412369166365430306, -0.6999999999999994005 ) ) ;
#10637=( LENGTH_UNIT ( ) NAMED_UNIT ( * ) SI_UNIT ( .MILLI., .METRE. ) );
#10656=CARTESIAN_POINT ( 'NONE',  ( 1.265035515811500089, -4.453021097817299712, -21.79535708920000658 ) ) ;
#10670=CARTESIAN_POINT ( 'NONE',  ( 0.07512830594656044747, -4.346272141329931671, -33.41110030499999795 ) ) ;
#10685=CARTESIAN_POINT ( 'NONE',  ( -4.939834082512651214, 0.8134902471039170413, -0.6999999999999992895 ) ) ;
#10691=CARTESIAN_POINT ( 'NONE',  ( 1.888485499342153151, 5.773790730162923879, -11.07047964830000453 ) ) ;
#10692=CARTESIAN_POINT ( 'NONE',  ( 6.379535387291454640, -1.442012952481606991, -32.18377053310000946 ) ) ;
#10697=CARTESIAN_POINT ( 'NONE',  ( 0.6138679561251692007, 4.311712124478117580, -29.00600711720001357 ) ) ;
#10727=CARTESIAN_POINT ( 'NONE',  ( 0.7444716670016126026, -5.443307122690507427, -1.373124048000001984 ) ) ;
#10728=CARTESIAN_POINT ( 'NONE',  ( -4.663991843195165465, -3.413757688390889555, -18.87254627010000263 ) ) ;
#10743=CARTESIAN_POINT ( 'NONE',  ( 6.034652528523337445, 2.501332855249893683, -11.49261350020000449 ) ) ;
#10751=ORIENTED_EDGE ( 'NONE', *, *, #1046, .T. ) ;
#10767=CARTESIAN_POINT ( 'NONE',  ( 4.880902371519058036, -3.592936783560450653, -8.972776792900004850 ) ) ;
#10777=EDGE_CURVE ( 'NONE', #3989, #23963, #27292, .T. ) ;
#10819=CARTESIAN_POINT ( 'NONE',  ( 3.653275382406360627, -2.426579979385206531, -0.6999999999999992895 ) ) ;
#10837=CARTESIAN_POINT ( 'NONE',  ( 6.379535387291454640, -1.442012952481606991, -32.78377053309999667 ) ) ;
#10852=CARTESIAN_POINT ( 'NONE',  ( -3.950843061919687038, 0.4864325623484713201, -0.6999999999999994005 ) ) ;
#10853=CARTESIAN_POINT ( 'NONE',  ( 6.105340317846409626, -0.2107885887935728730, -2.685409721200002320 ) ) ;
#10858=CARTESIAN_POINT ( 'NONE',  ( -6.108812354267502798, 0.1812703649498176306, -13.18304957890000040 ) ) ;
#10859=CARTESIAN_POINT ( 'NONE',  ( 0.09516252086846690994, -5.505278045713965618, -32.41110030500000505 ) ) ;
#10892=CARTESIAN_POINT ( 'NONE',  ( 1.213582369797474136, 4.521795443253902924, -2.553410702900004825 ) ) ;
#10893=CARTESIAN_POINT ( 'NONE',  ( -4.430040892179083478, 1.363067613765873931, -22.32289663399999924 ) ) ;
#10908=CARTESIAN_POINT ( 'NONE',  ( 3.256742448429973624, 4.730705660258329281, -17.21259163649999735 ) ) ;
#10929=CARTESIAN_POINT ( 'NONE',  ( 5.967946066639521874, -1.056419632483374116, -8.771482634700005221 ) ) ;
#10972=CARTESIAN_POINT ( 'NONE',  ( 3.843630909669756957, -2.553018000905745044, -0.6999999999999992895 ) ) ;
#10990=CARTESIAN_POINT ( 'NONE',  ( -5.496316421720869982, 0.7952554554161578304, -35.25783976330000513 ) ) ;
#11007=CARTESIAN_POINT ( 'NONE',  ( -0.9973419271877559389, -5.413498265897602302, -2.525234013000000832 ) ) ;
#11010=CARTESIAN_POINT ( 'NONE',  ( -1.499765329346335108, -5.740821375879678001, -13.55022317839999424 ) ) ;
#11031=CARTESIAN_POINT ( 'NONE',  ( -0.8540969733681119669, -5.154519737500188548, -0.7000226888021040539 ) ) ;
#11044=CARTESIAN_POINT ( 'NONE',  ( 2.604168029909177839, 2.875036802038033024, -35.70000000000000284 ) ) ;
#11050=CARTESIAN_POINT ( 'NONE',  ( 3.206179479465854243, -3.994457159022797299, -4.042821867100004241 ) ) ;
#11051=CARTESIAN_POINT ( 'NONE',  ( -4.215937884789282108, -1.105999120962573246, -24.54656121680000069 ) ) ;
#11065=CARTESIAN_POINT ( 'NONE',  ( 5.967946066722823240, -1.056419632538704967, -8.771482634700005221 ) ) ;
#11089=CARTESIAN_POINT ( 'NONE',  ( -4.992376002538913227, -2.377191163338420843, -11.97655742010000957 ) ) ;
#11144=CARTESIAN_POINT ( 'NONE',  ( 2.384687176691703936, 5.016209330407524369, -33.15113063600001198 ) ) ;
#11160=CARTESIAN_POINT ( 'NONE',  ( -4.646804529178781173, -0.2974863596997279203, -4.148838774900000637 ) ) ;
#11162=CARTESIAN_POINT ( 'NONE',  ( 1.002713911322309359, 3.977955482547946620, -17.55080441500000177 ) ) ;
#11163=CARTESIAN_POINT ( 'NONE',  ( 4.417684705200791484, 4.247747620870205409, -35.32341724620000178 ) ) ;
#11198=CARTESIAN_POINT ( 'NONE',  ( 5.763395275750641922, -2.111988417859953504, -6.436105321699997717 ) ) ;
#11199=CARTESIAN_POINT ( 'NONE',  ( 4.700333466414979178, 3.591691549163662511, -22.36727430110000725 ) ) ;
#11218=CARTESIAN_POINT ( 'NONE',  ( 0.3233900739386466605, 6.101867874933233793, -22.94418644579999977 ) ) ;
#11232=( GEOMETRIC_REPRESENTATION_CONTEXT ( 3 ) GLOBAL_UNCERTAINTY_ASSIGNED_CONTEXT ( ( #18816 ) ) GLOBAL_UNIT_ASSIGNED_CONTEXT ( ( #26854, #25973, #23464 ) ) REPRESENTATION_CONTEXT ( 'NONE', 'WORKASPACE' ) );
#11239=CARTESIAN_POINT ( 'NONE',  ( -1.657635364023947400, -6.345118362804027079, -11.95022317840000525 ) ) ;
#11320=CARTESIAN_POINT ( 'NONE',  ( -4.528911865900279388, -2.588562295002507785, -0.6999999999999992895 ) ) ;
#11321=CARTESIAN_POINT ( 'NONE',  ( -5.885952403586735215, -0.3768160556055083488, -3.148838774900004189 ) ) ;
#11326=CARTESIAN_POINT ( 'NONE',  ( -5.420006065778396831, -1.021773059489365032, -17.09949426530000238 ) ) ;
#11327=CARTESIAN_POINT ( 'NONE',  ( -3.850850186879767545, -3.402327863231305205, -32.89697003410000065 ) ) ;
#11347=CARTESIAN_POINT ( 'NONE',  ( 3.372732847734490225, -1.748957314603980739, -35.69999999999999574 ) ) ;
#11359=CARTESIAN_POINT ( 'NONE',  ( -4.273751495587445604, 4.364932658710685587, -5.168732180600002835 ) ) ;
#11360=CARTESIAN_POINT ( 'NONE',  ( 4.275653884846098762, -3.504702130532165505, -22.99674734060000958 ) ) ;
#11378=CARTESIAN_POINT ( 'NONE',  ( 5.503465972401561324, -2.627571514393519436, -20.88180150029999993 ) ) ;
#11399=CARTESIAN_POINT ( 'NONE',  ( -5.517889265940039145, -2.627421812126006451, -12.97655742010000246 ) ) ;
#11458=CARTESIAN_POINT ( 'NONE',  ( 3.123710955063051298, -2.074832491810060020, -35.95875473020000612 ) ) ;
#11475=CARTESIAN_POINT ( 'NONE',  ( -3.885731905334990799, 2.027028853511393613, -1.418764356299999418 ) ) ;
#11480=CARTESIAN_POINT ( 'NONE',  ( 1.270104287659547859, 5.038743611242932907, -18.05080441500000532 ) ) ;
#11514=CARTESIAN_POINT ( 'NONE',  ( 3.194067125856711264, 4.998308969841025906, -6.200967428500008261 ) ) ;
#11515=CARTESIAN_POINT ( 'NONE',  ( -4.555585884337687297, -4.059738318096004939, -24.84101932450000305 ) ) ;
#11520=CARTESIAN_POINT ( 'NONE',  ( -2.017871889752692383, -3.161030873707806332, -0.6999999999999992895 ) ) ;
#11532=DIRECTION ( 'NONE',  ( 0.000000000000000000, 0.000000000000000000, 1.000000000000000000 ) ) ;
#11534=EDGE_LOOP ( 'NONE', ( #22875, #27732 ) ) ;
#11556=CARTESIAN_POINT ( 'NONE',  ( 1.387648159808060999, -4.113210426322157609, -15.26414732020000464 ) ) ;
#11625=CARTESIAN_POINT ( 'NONE',  ( 2.032938288397245330, -5.563452252945958243, -5.260585232200003070 ) ) ;
#11630=CARTESIAN_POINT ( 'NONE',  ( 3.256742448429973624, 4.730705660258329281, -17.21259163649999735 ) ) ;
#11648=CARTESIAN_POINT ( 'NONE',  ( -0.3681746154257226067, -5.199302247677223932, -0.7000416189860052540 ) ) ;
#11660=CARTESIAN_POINT ( 'NONE',  ( 1.960433969464639770, 3.445019499235556282, -35.70000000000000284 ) ) ;
#11668=CARTESIAN_POINT ( 'NONE',  ( 1.604951280288046567, -4.392199147046019547, -6.760585232199999517 ) ) ;
#11669=CARTESIAN_POINT ( 'NONE',  ( -5.367600138795724618, 3.713494282866228069, -25.46779765530001072 ) ) ;
#11683=DIRECTION ( 'NONE',  ( 0.5532886644841251700, 0.8329895880221872551, -0.000000000000000000 ) ) ;
#11701=CARTESIAN_POINT ( 'NONE',  ( 3.580158647405435435, -3.257180914152149054, -0.6998395211047659936 ) ) ;
#11705=CARTESIAN_POINT ( 'NONE',  ( 5.093259405240584847, 0.3640143666580218373, -13.70704535869999852 ) ) ;
#11781=CARTESIAN_POINT ( 'NONE',  ( -3.993179150428259661, -2.644027878211168581, -5.952429326000007848 ) ) ;
#11786=CARTESIAN_POINT ( 'NONE',  ( 5.864965375735811115, 0.4191680585659274261, -15.64454535870001095 ) ) ;
#11816=CARTESIAN_POINT ( 'NONE',  ( 0.8664230844016814759, 4.728695873782988279, -35.70000000000000995 ) ) ;
#11827=CARTESIAN_POINT ( 'NONE',  ( 3.530284718056032833, 5.524446756132658898, -5.800967428500003464 ) ) ;
#11828=CARTESIAN_POINT ( 'NONE',  ( -3.357682761866084498, 3.860481585313637609, -27.64978588869999854 ) ) ;
#11834=CARTESIAN_POINT ( 'NONE',  ( 3.950106903291103588, 1.853988655799144958, -2.479170051700008148 ) ) ;
#11861=CARTESIAN_POINT ( 'NONE',  ( -5.295622588438499534, 1.541709225419852780, -15.30443125760000100 ) ) ;
#11916=CARTESIAN_POINT ( 'NONE',  ( 3.956700543085249322, -2.628121156294186633, -36.95875473020000612 ) ) ;
#11931=CARTESIAN_POINT ( 'NONE',  ( 0.2164205762250857590, 5.520452575866341860, -6.937690181099999798 ) ) ;
#11936=CARTESIAN_POINT ( 'NONE',  ( 3.931047123110473329, -1.876836795983962469, -20.88180150029999993 ) ) ;
#11967=CARTESIAN_POINT ( 'NONE',  ( 0.5618833952078471361, 4.215050809562369771, -35.70000000000000284 ) ) ;
#11970=CARTESIAN_POINT ( 'NONE',  ( -2.993757627400086552, -2.302355992395527018, -0.6999999999999990674 ) ) ;
#11973=CARTESIAN_POINT ( 'NONE',  ( -5.857861475075242019, -1.837656413297739766, -10.02323088899999881 ) ) ;
#11974=CARTESIAN_POINT ( 'NONE',  ( -1.611722395286938170, -6.291674585240492057, -27.54882611459999353 ) ) ;
#11980=CARTESIAN_POINT ( 'NONE',  ( -2.624260084387257219, -3.463915187244964056, -3.728945369300004753 ) ) ;
#12010=CARTESIAN_POINT ( 'NONE',  ( 2.970736324804301720, -3.997174458241568917, -0.6999965274516192215 ) ) ;
#12015=CARTESIAN_POINT ( 'NONE',  ( -2.227024806490486508, -3.476280271252723431, -18.70544088819999118 ) ) ;
#12043=CARTESIAN_POINT ( 'NONE',  ( -5.430430790592723156, -2.746024268427175841, -27.96472909260000606 ) ) ;
#12085=CARTESIAN_POINT ( 'NONE',  ( 5.506451109007332256, 0.7220432749125509364, -4.626979598400001947 ) ) ;
#12090=CARTESIAN_POINT ( 'NONE',  ( -6.228182343209494043, 0.8662545139425728014, -19.25159460730001371 ) ) ;
#12102=CARTESIAN_POINT ( 'NONE',  ( -4.274658871253808279, -0.8336587121505223408, -31.59652066320000330 ) ) ;
#12115=CARTESIAN_POINT ( 'NONE',  ( 3.748453146079709697, -2.489798990173139437, -0.6999999999999992895 ) ) ;
#12117=CARTESIAN_POINT ( 'NONE',  ( 1.101338864442481968, 3.961910147693631590, -35.69999999999999574 ) ) ;
#12125=CARTESIAN_POINT ( 'NONE',  ( 4.689100480956518879, -0.8300439969826994835, -9.708982634699996339 ) ) ;
#12126=CARTESIAN_POINT ( 'NONE',  ( 6.118976883090258667, 2.212479739890888197, -26.51249766020000109 ) ) ;
#12132=CARTESIAN_POINT ( 'NONE',  ( 1.348918213770415653, 4.124136235849971577, -11.07047964830000453 ) ) ;
#12159=CARTESIAN_POINT ( 'NONE',  ( 3.380278521335310593, -3.553170434758972096, -0.6997606425626067272 ) ) ;
#12163=CARTESIAN_POINT ( 'NONE',  ( 3.800013225884300905, -1.579422177728472487, -17.37122516810000405 ) ) ;
#12171=CARTESIAN_POINT ( 'NONE',  ( 6.379024725906915272, -4.237078256518207908, -35.69999999999999574 ) ) ;
#12186=CARTESIAN_POINT ( 'NONE',  ( -0.4514894588696777289, 4.335480228600245844, -25.88903409329999761 ) ) ;
#12237=CARTESIAN_POINT ( 'NONE',  ( -4.484282906631563925, 1.269983465873031347, -6.810827254900003958 ) ) ;
#12242=CARTESIAN_POINT ( 'NONE',  ( -4.448701673712592175, 0.6187532242676700989, -19.75159460729999950 ) ) ;
#12260=CARTESIAN_POINT ( 'NONE',  ( 3.999349870826697018, -3.799712354642017509, -31.05126389020000133 ) ) ;
#12275=CARTESIAN_POINT ( 'NONE',  ( 1.232334062959267840, 4.717565258337718781, -35.70000000000000284 ) ) ;
#12285=CARTESIAN_POINT ( 'NONE',  ( -5.530047734074942767, 3.478668956039820959, -10.44547590279999660 ) ) ;
#12286=CARTESIAN_POINT ( 'NONE',  ( -1.151230282303593366, -4.494053275198268693, -27.54882611460000774 ) ) ;
#12294=CARTESIAN_POINT ( 'NONE',  ( 0.3624384587677526026, -4.645391411234340850, -9.393384211799999051 ) ) ;
#12299=CARTESIAN_POINT ( 'NONE',  ( -1.058439502263211374, 6.005994971325610443, -19.83583244400000112 ) ) ;
#12306=AXIS2_PLACEMENT_3D ( 'NONE', #1938, #11683, #11532 ) ;
#12326=CARTESIAN_POINT ( 'NONE',  ( -5.420006065778396831, -1.021773059489365032, -15.09949426530000238 ) ) ;
#12351=CARTESIAN_POINT ( 'NONE',  ( 2.193772516446764076, 5.694542648089183423, -26.69462237479999800 ) ) ;
#12394=CARTESIAN_POINT ( 'NONE',  ( 0.5074138422395748638, -6.503547975687064664, -8.793384211800002959 ) ) ;
#12399=CARTESIAN_POINT ( 'NONE',  ( 3.736517203680826515, 4.566916950137848374, -21.25622222230000347 ) ) ;
#12411=CARTESIAN_POINT ( 'NONE',  ( -3.052438874386679046, 3.509528713898351970, -29.08728588869999498 ) ) ;
#12427=CARTESIAN_POINT ( 'NONE',  ( 0.5710670605986443160, 4.210710561773831628, -35.70000000000000284 ) ) ;
#12432=CARTESIAN_POINT ( 'NONE',  ( 5.067327387632984959, 4.072231104569050686, -8.354586407999999409 ) ) ;
#12433=CARTESIAN_POINT ( 'NONE',  ( -1.458225024262878255, -5.692467481908745519, -26.54882611460000419 ) ) ;
#12438=CARTESIAN_POINT ( 'NONE',  ( 4.310466091822805268, 1.786666325167808544, -11.49261350019999739 ) ) ;
#12470=CARTESIAN_POINT ( 'NONE',  ( -2.970579505556664834, -5.081274235795743444, -14.68182079290001241 ) ) ;
#12479=DIRECTION ( 'NONE',  ( -0.5532886644841250590, -0.8329895880221872551, 0.000000000000000000 ) ) ;
#12497=CARTESIAN_POINT ( 'NONE',  ( 4.801822465207213675, -2.670409256638542672, -27.93037294500000201 ) ) ;
#12516=CARTESIAN_POINT ( 'NONE',  ( 2.418887229898759816, -3.215241712391042839, -0.6999999999999992895 ) ) ;
#12546=CARTESIAN_POINT ( 'NONE',  ( -3.925562765917044228, -3.929887376319241898, -8.813991631000002158 ) ) ;
#12552=CARTESIAN_POINT ( 'NONE',  ( -3.679974273075529823, -2.251605409995534490, -21.90799200640000777 ) ) ;
#12566=CARTESIAN_POINT ( 'NONE',  ( -4.781258647701263520, -0.007971864669480827059, -29.10606466010000304 ) ) ;
#12582=CARTESIAN_POINT ( 'NONE',  ( -5.076643603551637796, -0.7187466731379940077, -0.6999999999999992895 ) ) ;
#12583=CARTESIAN_POINT ( 'NONE',  ( 3.436082050571401147, -2.282315740991585962, 0.9787452697999995399 ) ) ;
#12586=CARTESIAN_POINT ( 'NONE',  ( -0.8919388126321509125, 6.008950160842678301, -10.86772091660000150 ) ) ;
#12587=CARTESIAN_POINT ( 'NONE',  ( 5.771960588457029750, -1.304678385547908492, -31.78377053309999312 ) ) ;
#12595=CARTESIAN_POINT ( 'NONE',  ( -0.7188231668698794596, 4.425078454789642457, -34.84333403589999278 ) ) ;
#12623=CARTESIAN_POINT ( 'NONE',  ( 4.790228392454985773, 0.1193559191107074896, -19.73911200060000937 ) ) ;
#12650=CARTESIAN_POINT ( 'NONE',  ( 6.118976883090258667, 2.212479739890888197, -27.11249766020000607 ) ) ;
#12670=CARTESIAN_POINT ( 'NONE',  ( 3.555845164255195368, -2.474081261589745839, -0.6999999999999992895 ) ) ;
#12702=CARTESIAN_POINT ( 'NONE',  ( -4.661300745825158742, -2.852033519363592173, -22.90799200640000777 ) ) ;
#12716=( BOUNDED_SURFACE ( )  B_SPLINE_SURFACE ( 5, 5, ( 
 ( #27216, #29574, #12583, #17752, #5656, #15255 ),
 ( #10083, #29418, #5811, #26914, #3442, #19678 ),
 ( #5351, #14956, #24554, #13045, #22191, #22652 ),
 ( #7854, #1095, #29882, #27515, #1876, #5961 ),
 ( #21077, #1413, #27989, #30036, #4079, #15711 ),
 ( #11475, #23279, #25801, #18066, #6434, #30195 ),
 ( #25324, #16033, #25649, #15883, #30361, #13675 ),
 ( #17908, #1256, #25486, #15555, #18547, #6589 ),
 ( #8469, #18223, #18393, #8948, #20919, #8313 ),
 ( #13191, #25165, #3597, #16187, #3766, #10853 ),
 ( #8625, #1722, #22805, #27671, #20439, #6117 ),
 ( #3922, #13358, #22966, #11007, #20597, #23131 ),
 ( #4235, #20754, #13516, #27831, #6282, #1572 ),
 ( #11160, #28149, #8789, #11321, #30521, #13835 ),
 ( #23447, #18860, #30674, #16647, #28923, #14613 ),
 ( #18700, #19173, #9575, #16802, #4696, #9100 ),
 ( #23912, #28299, #28617, #6743, #14147, #2497 ),
 ( #28759, #4544, #16344, #12085, #25952, #7367 ),
 ( #26416, #4389, #13994, #7056, #14459, #9723 ),
 ( #23752, #5005, #24202, #11625, #24058, #9251 ),
 ( #21386, #26107, #21694, #26258, #2191, #142 ),
 ( #14305, #21223, #11781, #16959, #23601, #2643 ),
 ( #19330, #12237, #30978, #7213, #30823, #4858 ),
 ( #2347, #6892, #2037, #9410, #26564, #19014 ),
 ( #28458, #16320, #16495, #11931, #21539, #9883 ),
 ( #25250, #460, #7662, #8389, #6201, #17988 ),
 ( #22152, #17265, #26872, #8551, #10042, #10929 ),
 ( #5149, #19636, #5315, #29221, #14919, #10767 ),
 ( #24515, #608, #6040, #26713, #12394, #7517 ),
 ( #10195, #2952, #17418, #12546, #25093, #15803 ),
 ( #19795, #29378, #18149, #5882, #15489, #7820 ),
 ( #27754, #27026, #20368, #3524, #27600, #13121 ),
 ( #29960, #22728, #1177, #15639, #3682, #305 ),
 ( #13281, #29072, #1335, #20522, #22892, #22004 ),
 ( #30123, #25416, #3848, #21854, #14762, #19485 ),
 ( #17112, #24360, #2802, #30279, #28071, #13754 ),
 ( #18317, #4005, #8711, #1497, #23371, #18473 ),
 ( #20845, #30448, #1810, #8868, #11239, #20998 ),
 ( #28224, #27921, #30603, #11089, #21152, #11399 ),
 ( #26184, #6988, #6363, #9177, #20684, #4319 ),
 ( #6517, #13437, #16114, #16424, #25726, #4161 ),
 ( #30749, #18627, #23053, #18779, #6667, #15960 ),
 ( #25568, #9029, #26034, #30909, #23527, #16265 ),
 ( #4474, #13601, #11705, #23207, #28388, #1649 ),
 ( #25883, #6826, #23678, #13916, #1963, #18938 ),
 ( #11556, #14075, #2113, #21307, #9337, #28539 ),
 ( #16576, #19253, #19567, #12470, #2276, #2424 ),
 ( #21772, #382, #24280, #12326, #4932, #226 ),
 ( #29302, #31060, #9968, #11861, #26644, #19410 ),
 ( #17350, #7297, #7598, #28839, #73, #7745 ),
 ( #4620, #5083, #7447, #29151, #16885, #19723 ),
 ( #14542, #2729, #23832, #14225, #29000, #21464 ),
 ( #26489, #24135, #26341, #9498, #14691, #2574 ),
 ( #17191, #12163, #21933, #19099, #28694, #9812 ),
 ( #16721, #26794, #7139, #17042, #4789, #14386 ),
 ( #5238, #9651, #14853, #24444, #23985, #2878 ),
 ( #12015, #21620, #22085, #542, #10123, #20022 ),
 ( #17502, #22693, #3181, #6004, #30085, #10728 ),
 ( #5541, #25054, #17646, #1136, #12785, #3486 ),
 ( #3331, #17799, #13082, #27410, #5391, #19878 ),
 ( #3030, #15603, #25206, #12938, #27559, #838 ),
 ( #15146, #3640, #5848, #10278, #24746, #10430 ),
 ( #29619, #15452, #12623, #8051, #27258, #20328 ),
 ( #27107, #22234, #14998, #5695, #15302, #22548 ),
 ( #22394, #24906, #991, #10582, #20176, #29927 ),
 ( #29461, #29766, #24597, #8198, #8510, #8353 ),
 ( #17948, #13235, #26954, #22851, #690, #1299 ),
 ( #10893, #20484, #7896, #23325, #30871, #18434 ),
 ( #6159, #21267, #1770, #27713, #25844, #1610 ),
 ( #8671, #13399, #8991, #28031, #3964, #23485 ),
 ( #18591, #18111, #15761, #11199, #13717, #30238 ),
 ( #8829, #13562, #21117, #4120, #20801, #1923 ),
 ( #25373, #15920, #3812, #11360, #13878, #6630 ),
 ( #20957, #2077, #28187, #6476, #23169, #4434 ),
 ( #30563, #16229, #25528, #23010, #16077, #11515 ),
 ( #4281, #11051, #30713, #30408, #20642, #25689 ),
 ( #14038, #9140, #27880, #18743, #28344, #11669 ),
 ( #1458, #18269, #6790, #16386, #25994, #6325 ),
 ( #23640, #14189, #2838, #16540, #7561, #16688 ),
 ( #23954, #28797, #9456, #28655, #31020, #12126 ),
 ( #4581, #7260, #16850, #4747, #26299, #14353 ),
 ( #26149, #26758, #21732, #26456, #7102, #23791 ),
 ( #12286, #21586, #19529, #12433, #2389, #11974 ),
 ( #5194, #4899, #33, #9301, #9615, #14656 ),
 ( #17006, #7407, #14503, #184, #26608, #9772 ),
 ( #2237, #24100, #11828, #29117, #17152, #2538 ),
 ( #19215, #28499, #24244, #21899, #22051, #346 ),
 ( #18902, #21429, #14810, #19375, #19060, #28965 ),
 ( #5048, #2686, #9928, #24406, #6944, #26918 ),
 ( #8014, #27067, #7857, #17461, #19983, #5505 ),
 ( #17612, #8161, #15260, #14960, #27220, #19681 ),
 ( #5661, #13197, #25170, #5355, #27377, #7706 ),
 ( #24870, #15112, #501, #3144, #3447, #24706 ),
 ( #3602, #12742, #10087, #957, #3298, #5816 ),
 ( #15561, #12902, #29266, #802, #29733, #17312 ),
 ( #22510, #24559, #17757, #22355, #10392, #22195 ),
 ( #10547, #29578, #20142, #15414, #25014, #13049 ),
 ( #2997, #22656, #1099, #12587, #10692, #652 ),
 ( #10239, #19841, #29423, #20286, #29889, #8317 ),
 ( #17912, #27520, #5966, #10859, #16349, #20444 ),
 ( #4394, #15887, #11327, #13363, #18553, #30199 ),
 ( #8630, #18071, #1577, #6595, #25490, #25808 ),
 ( #18227, #25958, #6287, #22809, #23285, #25654 ),
 ( #3928, #6750, #27994, #1262, #23135, #20924 ),
 ( #30042, #6439, #8475, #30526, #13522, #11163 ),
 ( #27676, #6122, #20760, #16192, #1882, #20602 ),
 ( #28305, #15716, #3772, #4240, #1418, #27835 ),
 ( #30365, #13842, #8794, #18397, #23452, #30679 ) ),
 .UNSPECIFIED., .F., .F., .T. ) 
 B_SPLINE_SURFACE_WITH_KNOTS ( ( 6, 3, 3, 3, 3, 3, 3, 3, 3, 3, 3, 3, 3, 3, 3, 3, 3, 3, 3, 3, 3, 3, 3, 3, 3, 3, 3, 3, 3, 3, 3, 3, 3, 3, 3, 6 ),
 ( 6, 6 ),
 ( 0.000000000000000000, 11.38862009670000042, 23.17260734259999921, 34.79167593860000096, 46.25425528950000142, 57.87229377410000097, 69.67120816000000616, 81.20502170430000888, 92.80704244429999505, 104.1208912059999960, 115.9269080290000034, 127.3307717769999954, 139.1306782750000082, 150.7654282180000109, 162.2434640489999822, 173.6637378899999931, 185.2020570420000070, 194.1769840820000184, 203.3038760180000111, 212.5853790139999830, 224.1393301889999918, 235.6932813650000185, 246.8715721779999797, 258.4996770380000157, 270.1277818960000445, 281.7035649139999691, 293.2822232819999613, 304.6732510989999696, 316.1434960830000023, 327.6894369340000139, 339.2353777880000507, 350.7813186390000055, 362.5843219139999860, 374.0573691039999744, 385.8560256170000002, 397.5961180479999939 ),
 ( 0.000000000000000000, 8.337129679329999377 ),
 .UNSPECIFIED. ) 
 GEOMETRIC_REPRESENTATION_ITEM ( )  RATIONAL_B_SPLINE_SURFACE ( (
 ( 1.000000000000000000, 0.5999999999999999778, 0.4000000000000000222, 0.2999999999999999889, 0.2500000000000000000, 0.2500000000000000000),
 ( 1.000000000000000000, 0.5999999999999999778, 0.4000000000000000222, 0.2999999999999999889, 0.2500000000000000000, 0.2500000000000000000),
 ( 1.000000000000000000, 0.5999999999999999778, 0.4000000000000000222, 0.2999999999999999889, 0.2500000000000000000, 0.2500000000000000000),
 ( 1.000000000000000000, 0.5999999999999999778, 0.4000000000000000222, 0.2999999999999999889, 0.2500000000000000000, 0.2500000000000000000),
 ( 1.000000000000000000, 0.5999999999999999778, 0.4000000000000000222, 0.2999999999999999889, 0.2500000000000000000, 0.2500000000000000000),
 ( 1.000000000000000000, 0.5999999999999999778, 0.4000000000000000222, 0.2999999999999999889, 0.2500000000000000000, 0.2500000000000000000),
 ( 1.000000000000000000, 0.5999999999999999778, 0.4000000000000000222, 0.2999999999999999889, 0.2500000000000000000, 0.2500000000000000000),
 ( 1.000000000000000000, 0.5999999999999999778, 0.4000000000000000222, 0.2999999999999999889, 0.2500000000000000000, 0.2500000000000000000),
 ( 1.000000000000000000, 0.5999999999999999778, 0.4000000000000000222, 0.2999999999999999889, 0.2500000000000000000, 0.2500000000000000000),
 ( 1.000000000000000000, 0.5999999999999999778, 0.4000000000000000222, 0.2999999999999999889, 0.2500000000000000000, 0.2500000000000000000),
 ( 1.000000000000000000, 0.5999999999999999778, 0.4000000000000000222, 0.2999999999999999889, 0.2500000000000000000, 0.2500000000000000000),
 ( 1.000000000000000000, 0.5999999999999999778, 0.4000000000000000222, 0.2999999999999999889, 0.2500000000000000000, 0.2500000000000000000),
 ( 1.000000000000000000, 0.5999999999999999778, 0.4000000000000000222, 0.2999999999999999889, 0.2500000000000000000, 0.2500000000000000000),
 ( 1.000000000000000000, 0.5999999999999999778, 0.4000000000000000222, 0.2999999999999999889, 0.2500000000000000000, 0.2500000000000000000),
 ( 1.000000000000000000, 0.5999999999999999778, 0.4000000000000000222, 0.2999999999999999889, 0.2500000000000000000, 0.2500000000000000000),
 ( 1.000000000000000000, 0.5999999999999999778, 0.4000000000000000222, 0.2999999999999999889, 0.2500000000000000000, 0.2500000000000000000),
 ( 1.000000000000000000, 0.5999999999999999778, 0.4000000000000000222, 0.2999999999999999889, 0.2500000000000000000, 0.2500000000000000000),
 ( 1.000000000000000000, 0.5999999999999999778, 0.4000000000000000222, 0.2999999999999999889, 0.2500000000000000000, 0.2500000000000000000),
 ( 1.000000000000000000, 0.5999999999999999778, 0.4000000000000000222, 0.2999999999999999889, 0.2500000000000000000, 0.2500000000000000000),
 ( 1.000000000000000000, 0.5999999999999999778, 0.4000000000000000222, 0.2999999999999999889, 0.2500000000000000000, 0.2500000000000000000),
 ( 1.000000000000000000, 0.5999999999999999778, 0.4000000000000000222, 0.2999999999999999889, 0.2500000000000000000, 0.2500000000000000000),
 ( 1.000000000000000000, 0.5999999999999999778, 0.4000000000000000222, 0.2999999999999999889, 0.2500000000000000000, 0.2500000000000000000),
 ( 1.000000000000000000, 0.5999999999999999778, 0.4000000000000000222, 0.2999999999999999889, 0.2500000000000000000, 0.2500000000000000000),
 ( 1.000000000000000000, 0.5999999999999999778, 0.4000000000000000222, 0.2999999999999999889, 0.2500000000000000000, 0.2500000000000000000),
 ( 1.000000000000000000, 0.5999999999999999778, 0.4000000000000000222, 0.2999999999999999889, 0.2500000000000000000, 0.2500000000000000000),
 ( 1.000000000000000000, 0.5999999999999999778, 0.4000000000000000222, 0.2999999999999999889, 0.2500000000000000000, 0.2500000000000000000),
 ( 1.000000000000000000, 0.5999999999999999778, 0.4000000000000000222, 0.2999999999999999889, 0.2500000000000000000, 0.2500000000000000000),
 ( 1.000000000000000000, 0.5999999999999999778, 0.4000000000000000222, 0.2999999999999999889, 0.2500000000000000000, 0.2500000000000000000),
 ( 1.000000000000000000, 0.5999999999999999778, 0.4000000000000000222, 0.2999999999999999889, 0.2500000000000000000, 0.2500000000000000000),
 ( 1.000000000000000000, 0.5999999999999999778, 0.4000000000000000222, 0.2999999999999999889, 0.2500000000000000000, 0.2500000000000000000),
 ( 1.000000000000000000, 0.5999999999999999778, 0.4000000000000000222, 0.2999999999999999889, 0.2500000000000000000, 0.2500000000000000000),
 ( 1.000000000000000000, 0.5999999999999999778, 0.4000000000000000222, 0.2999999999999999889, 0.2500000000000000000, 0.2500000000000000000),
 ( 1.000000000000000000, 0.5999999999999999778, 0.4000000000000000222, 0.2999999999999999889, 0.2500000000000000000, 0.2500000000000000000),
 ( 1.000000000000000000, 0.5999999999999999778, 0.4000000000000000222, 0.2999999999999999889, 0.2500000000000000000, 0.2500000000000000000),
 ( 1.000000000000000000, 0.5999999999999999778, 0.4000000000000000222, 0.2999999999999999889, 0.2500000000000000000, 0.2500000000000000000),
 ( 1.000000000000000000, 0.5999999999999999778, 0.4000000000000000222, 0.2999999999999999889, 0.2500000000000000000, 0.2500000000000000000),
 ( 1.000000000000000000, 0.5999999999999999778, 0.4000000000000000222, 0.2999999999999999889, 0.2500000000000000000, 0.2500000000000000000),
 ( 1.000000000000000000, 0.5999999999999999778, 0.4000000000000000222, 0.2999999999999999889, 0.2500000000000000000, 0.2500000000000000000),
 ( 1.000000000000000000, 0.5999999999999999778, 0.4000000000000000222, 0.2999999999999999889, 0.2500000000000000000, 0.2500000000000000000),
 ( 1.000000000000000000, 0.5999999999999999778, 0.4000000000000000222, 0.2999999999999999889, 0.2500000000000000000, 0.2500000000000000000),
 ( 1.000000000000000000, 0.5999999999999999778, 0.4000000000000000222, 0.2999999999999999889, 0.2500000000000000000, 0.2500000000000000000),
 ( 1.000000000000000000, 0.5999999999999999778, 0.4000000000000000222, 0.2999999999999999889, 0.2500000000000000000, 0.2500000000000000000),
 ( 1.000000000000000000, 0.5999999999999999778, 0.4000000000000000222, 0.2999999999999999889, 0.2500000000000000000, 0.2500000000000000000),
 ( 1.000000000000000000, 0.5999999999999999778, 0.4000000000000000222, 0.2999999999999999889, 0.2500000000000000000, 0.2500000000000000000),
 ( 1.000000000000000000, 0.5999999999999999778, 0.4000000000000000222, 0.2999999999999999889, 0.2500000000000000000, 0.2500000000000000000),
 ( 1.000000000000000000, 0.5999999999999999778, 0.4000000000000000222, 0.2999999999999999889, 0.2500000000000000000, 0.2500000000000000000),
 ( 1.000000000000000000, 0.5999999999999999778, 0.4000000000000000222, 0.2999999999999999889, 0.2500000000000000000, 0.2500000000000000000),
 ( 1.000000000000000000, 0.5999999999999999778, 0.4000000000000000222, 0.2999999999999999889, 0.2500000000000000000, 0.2500000000000000000),
 ( 1.000000000000000000, 0.5999999999999999778, 0.4000000000000000222, 0.2999999999999999889, 0.2500000000000000000, 0.2500000000000000000),
 ( 1.000000000000000000, 0.5999999999999999778, 0.4000000000000000222, 0.2999999999999999889, 0.2500000000000000000, 0.2500000000000000000),
 ( 1.000000000000000000, 0.5999999999999999778, 0.4000000000000000222, 0.2999999999999999889, 0.2500000000000000000, 0.2500000000000000000),
 ( 1.000000000000000000, 0.5999999999999999778, 0.4000000000000000222, 0.2999999999999999889, 0.2500000000000000000, 0.2500000000000000000),
 ( 1.000000000000000000, 0.5999999999999999778, 0.4000000000000000222, 0.2999999999999999889, 0.2500000000000000000, 0.2500000000000000000),
 ( 1.000000000000000000, 0.5999999999999999778, 0.4000000000000000222, 0.2999999999999999889, 0.2500000000000000000, 0.2500000000000000000),
 ( 1.000000000000000000, 0.5999999999999999778, 0.4000000000000000222, 0.2999999999999999889, 0.2500000000000000000, 0.2500000000000000000),
 ( 1.000000000000000000, 0.5999999999999999778, 0.4000000000000000222, 0.2999999999999999889, 0.2500000000000000000, 0.2500000000000000000),
 ( 1.000000000000000000, 0.5999999999999999778, 0.4000000000000000222, 0.2999999999999999889, 0.2500000000000000000, 0.2500000000000000000),
 ( 1.000000000000000000, 0.5999999999999999778, 0.4000000000000000222, 0.2999999999999999889, 0.2500000000000000000, 0.2500000000000000000),
 ( 1.000000000000000000, 0.5999999999999999778, 0.4000000000000000222, 0.2999999999999999889, 0.2500000000000000000, 0.2500000000000000000),
 ( 1.000000000000000000, 0.5999999999999999778, 0.4000000000000000222, 0.2999999999999999889, 0.2500000000000000000, 0.2500000000000000000),
 ( 1.000000000000000000, 0.5999999999999999778, 0.4000000000000000222, 0.2999999999999999889, 0.2500000000000000000, 0.2500000000000000000),
 ( 1.000000000000000000, 0.5999999999999999778, 0.4000000000000000222, 0.2999999999999999889, 0.2500000000000000000, 0.2500000000000000000),
 ( 1.000000000000000000, 0.5999999999999999778, 0.4000000000000000222, 0.2999999999999999889, 0.2500000000000000000, 0.2500000000000000000),
 ( 1.000000000000000000, 0.5999999999999999778, 0.4000000000000000222, 0.2999999999999999889, 0.2500000000000000000, 0.2500000000000000000),
 ( 1.000000000000000000, 0.5999999999999999778, 0.4000000000000000222, 0.2999999999999999889, 0.2500000000000000000, 0.2500000000000000000),
 ( 1.000000000000000000, 0.5999999999999999778, 0.4000000000000000222, 0.2999999999999999889, 0.2500000000000000000, 0.2500000000000000000),
 ( 1.000000000000000000, 0.5999999999999999778, 0.4000000000000000222, 0.2999999999999999889, 0.2500000000000000000, 0.2500000000000000000),
 ( 1.000000000000000000, 0.5999999999999999778, 0.4000000000000000222, 0.2999999999999999889, 0.2500000000000000000, 0.2500000000000000000),
 ( 1.000000000000000000, 0.5999999999999999778, 0.4000000000000000222, 0.2999999999999999889, 0.2500000000000000000, 0.2500000000000000000),
 ( 1.000000000000000000, 0.5999999999999999778, 0.4000000000000000222, 0.2999999999999999889, 0.2500000000000000000, 0.2500000000000000000),
 ( 1.000000000000000000, 0.5999999999999999778, 0.4000000000000000222, 0.2999999999999999889, 0.2500000000000000000, 0.2500000000000000000),
 ( 1.000000000000000000, 0.5999999999999999778, 0.4000000000000000222, 0.2999999999999999889, 0.2500000000000000000, 0.2500000000000000000),
 ( 1.000000000000000000, 0.5999999999999999778, 0.4000000000000000222, 0.2999999999999999889, 0.2500000000000000000, 0.2500000000000000000),
 ( 1.000000000000000000, 0.5999999999999999778, 0.4000000000000000222, 0.2999999999999999889, 0.2500000000000000000, 0.2500000000000000000),
 ( 1.000000000000000000, 0.5999999999999999778, 0.4000000000000000222, 0.2999999999999999889, 0.2500000000000000000, 0.2500000000000000000),
 ( 1.000000000000000000, 0.5999999999999999778, 0.4000000000000000222, 0.2999999999999999889, 0.2500000000000000000, 0.2500000000000000000),
 ( 1.000000000000000000, 0.5999999999999999778, 0.4000000000000000222, 0.2999999999999999889, 0.2500000000000000000, 0.2500000000000000000),
 ( 1.000000000000000000, 0.5999999999999999778, 0.4000000000000000222, 0.2999999999999999889, 0.2500000000000000000, 0.2500000000000000000),
 ( 1.000000000000000000, 0.5999999999999999778, 0.4000000000000000222, 0.2999999999999999889, 0.2500000000000000000, 0.2500000000000000000),
 ( 1.000000000000000000, 0.5999999999999999778, 0.4000000000000000222, 0.2999999999999999889, 0.2500000000000000000, 0.2500000000000000000),
 ( 1.000000000000000000, 0.5999999999999999778, 0.4000000000000000222, 0.2999999999999999889, 0.2500000000000000000, 0.2500000000000000000),
 ( 1.000000000000000000, 0.5999999999999999778, 0.4000000000000000222, 0.2999999999999999889, 0.2500000000000000000, 0.2500000000000000000),
 ( 1.000000000000000000, 0.5999999999999999778, 0.4000000000000000222, 0.2999999999999999889, 0.2500000000000000000, 0.2500000000000000000),
 ( 1.000000000000000000, 0.5999999999999999778, 0.4000000000000000222, 0.2999999999999999889, 0.2500000000000000000, 0.2500000000000000000),
 ( 1.000000000000000000, 0.5999999999999999778, 0.4000000000000000222, 0.2999999999999999889, 0.2500000000000000000, 0.2500000000000000000),
 ( 1.000000000000000000, 0.5999999999999999778, 0.4000000000000000222, 0.2999999999999999889, 0.2500000000000000000, 0.2500000000000000000),
 ( 1.000000000000000000, 0.5999999999999999778, 0.4000000000000000222, 0.2999999999999999889, 0.2500000000000000000, 0.2500000000000000000),
 ( 1.000000000000000000, 0.5999999999999999778, 0.4000000000000000222, 0.2999999999999999889, 0.2500000000000000000, 0.2500000000000000000),
 ( 1.000000000000000000, 0.5999999999999999778, 0.4000000000000000222, 0.2999999999999999889, 0.2500000000000000000, 0.2500000000000000000),
 ( 1.000000000000000000, 0.5999999999999999778, 0.4000000000000000222, 0.2999999999999999889, 0.2500000000000000000, 0.2500000000000000000),
 ( 1.000000000000000000, 0.5999999999999999778, 0.4000000000000000222, 0.2999999999999999889, 0.2500000000000000000, 0.2500000000000000000),
 ( 1.000000000000000000, 0.5999999999999999778, 0.4000000000000000222, 0.2999999999999999889, 0.2500000000000000000, 0.2500000000000000000),
 ( 1.000000000000000000, 0.5999999999999999778, 0.4000000000000000222, 0.2999999999999999889, 0.2500000000000000000, 0.2500000000000000000),
 ( 1.000000000000000000, 0.5999999999999999778, 0.4000000000000000222, 0.2999999999999999889, 0.2500000000000000000, 0.2500000000000000000),
 ( 1.000000000000000000, 0.5999999999999999778, 0.4000000000000000222, 0.2999999999999999889, 0.2500000000000000000, 0.2500000000000000000),
 ( 1.000000000000000000, 0.5999999999999999778, 0.4000000000000000222, 0.2999999999999999889, 0.2500000000000000000, 0.2500000000000000000),
 ( 1.000000000000000000, 0.5999999999999999778, 0.4000000000000000222, 0.2999999999999999889, 0.2500000000000000000, 0.2500000000000000000),
 ( 1.000000000000000000, 0.5999999999999999778, 0.4000000000000000222, 0.2999999999999999889, 0.2500000000000000000, 0.2500000000000000000),
 ( 1.000000000000000000, 0.5999999999999999778, 0.4000000000000000222, 0.2999999999999999889, 0.2500000000000000000, 0.2500000000000000000),
 ( 1.000000000000000000, 0.5999999999999999778, 0.4000000000000000222, 0.2999999999999999889, 0.2500000000000000000, 0.2500000000000000000),
 ( 1.000000000000000000, 0.5999999999999999778, 0.4000000000000000222, 0.2999999999999999889, 0.2500000000000000000, 0.2500000000000000000),
 ( 1.000000000000000000, 0.5999999999999999778, 0.4000000000000000222, 0.2999999999999999889, 0.2500000000000000000, 0.2500000000000000000),
 ( 1.000000000000000000, 0.5999999999999999778, 0.4000000000000000222, 0.2999999999999999889, 0.2500000000000000000, 0.2500000000000000000),
 ( 1.000000000000000000, 0.5999999999999999778, 0.4000000000000000222, 0.2999999999999999889, 0.2500000000000000000, 0.2500000000000000000),
 ( 1.000000000000000000, 0.5999999999999999778, 0.4000000000000000222, 0.2999999999999999889, 0.2500000000000000000, 0.2500000000000000000),
 ( 1.000000000000000000, 0.5999999999999999778, 0.4000000000000000222, 0.2999999999999999889, 0.2500000000000000000, 0.2500000000000000000),
 ( 1.000000000000000000, 0.5999999999999999778, 0.4000000000000000222, 0.2999999999999999889, 0.2500000000000000000, 0.2500000000000000000),
 ( 1.000000000000000000, 0.5999999999999999778, 0.4000000000000000222, 0.2999999999999999889, 0.2500000000000000000, 0.2500000000000000000) ) ) 
 REPRESENTATION_ITEM ( '' )  SURFACE ( )  );
#12717=CARTESIAN_POINT ( 'NONE',  ( -2.308365619037861638, -4.044857084274060988, -31.17642233979999844 ) ) ;
#12737=CARTESIAN_POINT ( 'NONE',  ( -3.777365892340432296, 2.405994524213964425, -0.6999999999999989564 ) ) ;
#12741=CARTESIAN_POINT ( 'NONE',  ( -3.711147652395973662, 4.588201686596787177, -14.60352819870001007 ) ) ;
#12742=CARTESIAN_POINT ( 'NONE',  ( -4.188726303739424672, 1.192588472141205891, -30.80158078970000091 ) ) ;
#12748=CARTESIAN_POINT ( 'NONE',  ( 3.503437880484509659, 2.636891074944046398, -32.36032172559999509 ) ) ;
#12784=CARTESIAN_POINT ( 'NONE',  ( -3.885731905334990799, 2.027028853511393613, -1.418764356299999418 ) ) ;
#12785=CARTESIAN_POINT ( 'NONE',  ( -6.228182343209494043, 0.8662545139425728014, -18.65159460730000873 ) ) ;
#12835=CARTESIAN_POINT ( 'NONE',  ( 1.158713442569508478, -3.699378802302395908, -0.6999999999999992895 ) ) ;
#12865=CARTESIAN_POINT ( 'NONE',  ( 5.195105410215491659, 3.969764343816663210, -23.96727430110000157 ) ) ;
#12879=CARTESIAN_POINT ( 'NONE',  ( -0.4593365651765490831, 6.553622599173768215, -35.49518930509999848 ) ) ;
#12892=CARTESIAN_POINT ( 'NONE',  ( 2.327075022089611256, 4.449294111946768382, -35.69999999999998863 ) ) ;
#12896=CARTESIAN_POINT ( 'NONE',  ( -4.724067226770716665, 1.405641512842028762, -0.6999999999999991784 ) ) ;
#12901=CARTESIAN_POINT ( 'NONE',  ( 0.8539377161337347033, 4.705374660993639324, -14.96150681849999842 ) ) ;
#12902=CARTESIAN_POINT ( 'NONE',  ( -1.932773295258167545, 4.259541830411040841, -31.22635571289999845 ) ) ;
#12937=CARTESIAN_POINT ( 'NONE',  ( -5.440024667461782037, 2.837840394948672351, -2.018764356300002838 ) ) ;
#12938=CARTESIAN_POINT ( 'NONE',  ( -0.9576357401321299312, 5.433995450232204760, -18.83583244400000112 ) ) ;
#12953=CARTESIAN_POINT ( 'NONE',  ( -1.657635364023947400, -6.345118362804027079, -12.55022317840000312 ) ) ;
#12993=FILL_AREA_STYLE_COLOUR ( '', #28805 ) ;
#13014=CARTESIAN_POINT ( 'NONE',  ( -2.258375515285932167, 5.046176096966566327, -23.73780126170000315 ) ) ;
#13027=CARTESIAN_POINT ( 'NONE',  ( 2.831388952324535691, -5.386915550550475551, -33.20721934060000535 ) ) ;
#13040=CARTESIAN_POINT ( 'NONE',  ( 2.506562108457635940, 4.370859049088616111, -35.69999999999999574 ) ) ;
#13044=CARTESIAN_POINT ( 'NONE',  ( -3.813730490650353744, 1.734508981506462710, -0.6999999999999992895 ) ) ;
#13045=CARTESIAN_POINT ( 'NONE',  ( 0.7444716670016126026, -5.443307122690507427, 0.6268759519999975716 ) ) ;
#13048=CARTESIAN_POINT ( 'NONE',  ( 2.536150288113637963, -3.576595042060325635, -12.12388893670000201 ) ) ;
#13049=CARTESIAN_POINT ( 'NONE',  ( 4.904813032679735230, 3.691647504909488564, -32.36032172560000930 ) ) ;
#13081=CARTESIAN_POINT ( 'NONE',  ( -3.510061880997908279, 5.032561185093348044, -2.227651354100003367 ) ) ;
#13082=CARTESIAN_POINT ( 'NONE',  ( -2.879958020435939847, 3.829670441253783864, -18.69314294429999634 ) ) ;
#13121=CARTESIAN_POINT ( 'NONE',  ( -5.530047734074942767, 3.478668956039820959, -10.44547590279999660 ) ) ;
#13163=CARTESIAN_POINT ( 'NONE',  ( 1.265035515811502309, -4.453021097817297047, -21.29535708919999593 ) ) ;
#13176=CARTESIAN_POINT ( 'NONE',  ( -0.4155902256269943806, 5.929468065910143082, -35.89518930509999706 ) ) ;
#13190=CARTESIAN_POINT ( 'NONE',  ( -3.788551368745695314, 2.416708791688973790, -0.6999999999999992895 ) ) ;
#13191=CARTESIAN_POINT ( 'NONE',  ( 4.360957369889326252, -0.1505632777267507105, -2.685409721200002320 ) ) ;
#13196=CARTESIAN_POINT ( 'NONE',  ( -5.517889265940039145, -2.627421812126006451, -13.57655742009999855 ) ) ;
#13197=CARTESIAN_POINT ( 'NONE',  ( -2.308365619037861638, -4.044857084274060988, -30.17642233980000910 ) ) ;
#13203=CARTESIAN_POINT ( 'NONE',  ( -4.346598770676703083, -0.007247149673123010061, -28.16856466009999593 ) ) ;
#13234=CARTESIAN_POINT ( 'NONE',  ( 2.223383862040885450, -3.430296892840217993, -0.1659393883000001568 ) ) ;
#13235=CARTESIAN_POINT ( 'NONE',  ( -3.679974273075534708, -2.251605409995533602, -21.40799200640000066 ) ) ;
#13253=CARTESIAN_POINT ( 'NONE',  ( -3.283272085058491996, -5.616145207990252963, -15.68182079290000175 ) ) ;
#13281=CARTESIAN_POINT ( 'NONE',  ( 1.348918213770415653, 4.124136235849971577, -11.07047964830000453 ) ) ;
#13344=CARTESIAN_POINT ( 'NONE',  ( -4.976668802704899086, 3.592974922927941073, -34.46696136359999940 ) ) ;
#13358=CARTESIAN_POINT ( 'NONE',  ( -0.7873752056533391830, -4.273814420472604070, -3.025234013000003497 ) ) ;
#13362=CARTESIAN_POINT ( 'NONE',  ( 5.466312515054250198, -2.792605348973308477, -12.51474735220000412 ) ) ;
#13363=CARTESIAN_POINT ( 'NONE',  ( -4.434312336397093546, -3.917832084918029256, -32.83447003410000065 ) ) ;
#13391=CARTESIAN_POINT ( 'NONE',  ( 3.746497173757565413, -0.1670055334890632737, -35.69999999999999574 ) ) ;
#13398=CARTESIAN_POINT ( 'NONE',  ( 4.080592064681261455, -5.083854565965863159, -3.105321867100004241 ) ) ;
#13399=CARTESIAN_POINT ( 'NONE',  ( 0.2309929099465236890, 4.358477053493579056, -22.44418644580001043 ) ) ;
#13413=CARTESIAN_POINT ( 'NONE',  ( -2.825020644939634007, -4.425443225455641283, -0.6999999999999992895 ) ) ;
#13437=CARTESIAN_POINT ( 'NONE',  ( -2.929853409778804263, 3.622264489389753539, -13.10352819870000118 ) ) ;
#13480=CARTESIAN_POINT ( 'NONE',  ( 3.767248616521118976, -2.502283324777556661, -0.7105340489000482318 ) ) ;
#13499=CARTESIAN_POINT ( 'NONE',  ( 5.877945039781666381, 1.734296231098907182, -36.13159726780000369 ) ) ;
#13516=CARTESIAN_POINT ( 'NONE',  ( -2.886686092853935293, -3.810306705960904594, -2.791445369299998536 ) ) ;
#13521=CARTESIAN_POINT ( 'NONE',  ( 1.942707423728255778, -5.758494596869851989, -15.26414732020000464 ) ) ;
#13522=CARTESIAN_POINT ( 'NONE',  ( 4.417684705200791484, 4.247747620870205409, -34.72341724620000036 ) ) ;
#13538=CARTESIAN_POINT ( 'NONE',  ( -2.413485703671791605, -4.688120701072898910, -0.7000000000061800121 ) ) ;
#13561=CARTESIAN_POINT ( 'NONE',  ( -4.646804529178800713, -0.2974863596997128767, -4.648838774900006854 ) ) ;
#13562=CARTESIAN_POINT ( 'NONE',  ( 4.266075142677459908, -0.9221078188639819651, -23.29036215649999875 ) ) ;
#13578=CARTESIAN_POINT ( 'NONE',  ( 1.888485499342153151, 5.773790730162923879, -11.07047964830000453 ) ) ;
#13601=CARTESIAN_POINT ( 'NONE',  ( 4.630235822890138131, 0.3309221515414816350, -14.14454535870000029 ) ) ;
#13643=CARTESIAN_POINT ( 'NONE',  ( 3.728929371600147924, -2.476830901180399724, -0.7104894750999627417 ) ) ;
#13659=CARTESIAN_POINT ( 'NONE',  ( 4.051823674760414384, -0.6775361292690335047, -36.24517599850000948 ) ) ;
#13675=CARTESIAN_POINT ( 'NONE',  ( -3.510061880997908279, 5.032561185093348044, -1.627651354100000169 ) ) ;
#13680=CARTESIAN_POINT ( 'NONE',  ( -3.283272085064022239, -5.616145207998583189, -16.28182079290000672 ) ) ;
#13689=DIRECTION ( 'NONE',  ( 0.5532886644841251700, 0.8329895880221872551, -0.000000000000000000 ) ) ;
#13716=CARTESIAN_POINT ( 'NONE',  ( -2.624260084387262104, -3.463915187244965388, -4.228945369299999868 ) ) ;
#13717=CARTESIAN_POINT ( 'NONE',  ( 5.195105410215491659, 3.969764343816663210, -22.76727430110000938 ) ) ;
#13734=CARTESIAN_POINT ( 'NONE',  ( 5.323890883912177685, 1.532987191732344767, -35.53910482770000812 ) ) ;
#13754=CARTESIAN_POINT ( 'NONE',  ( 5.466312515054250198, -2.792605348973308477, -11.91474735220000092 ) ) ;
#13799=CARTESIAN_POINT ( 'NONE',  ( 4.213005042626035923, -2.798363829541613335, -35.30210069600008183 ) ) ;
#13835=CARTESIAN_POINT ( 'NONE',  ( -6.505526340832360255, -0.4164809035307331930, -4.148838774900000637 ) ) ;
#13841=CARTESIAN_POINT ( 'NONE',  ( 3.082386449366550707, -3.056625787687244689, -15.56112212870000278 ) ) ;
#13842=CARTESIAN_POINT ( 'NONE',  ( 3.123710955063047745, -2.074832491810059132, -35.45875473019999902 ) ) ;
#13877=CARTESIAN_POINT ( 'NONE',  ( -3.324062773583611907, -4.387625903868788591, -4.728945369300002532 ) ) ;
#13878=CARTESIAN_POINT ( 'NONE',  ( 4.725722714813314518, -3.873618144263061946, -23.39674734060000105 ) ) ;
#13894=CARTESIAN_POINT ( 'NONE',  ( 2.831388952324535691, -5.386915550550475551, -33.20721934060000535 ) ) ;
#13916=CARTESIAN_POINT ( 'NONE',  ( 3.904356169178446745, -3.871725997715349532, -14.06112212870000455 ) ) ;
#13994=CARTESIAN_POINT ( 'NONE',  ( 4.528382002446963206, -1.659419471228278375, -4.898605321699998072 ) ) ;
#13999=CARTESIAN_POINT ( 'NONE',  ( 4.543782907447139863, 1.343478130985185537, -18.47940840230000248 ) ) ;
#14015=DIRECTION ( 'NONE',  ( 0.000000000000000000, 0.000000000000000000, 1.000000000000000000 ) ) ;
#14016=CARTESIAN_POINT ( 'NONE',  ( 1.211329632739529982, -4.999378637410044846, -0.6999988961696247403 ) ) ;
#14037=CARTESIAN_POINT ( 'NONE',  ( 2.032938288397245330, -5.563452252945958243, -7.260585232200002181 ) ) ;
#14038=CARTESIAN_POINT ( 'NONE',  ( -3.834000099192893973, 2.652495916366584439, -25.46779765530001072 ) ) ;
#14053=CARTESIAN_POINT ( 'NONE',  ( 4.420334067734101424, -4.199682076162645217, -30.05126389020000488 ) ) ;
#14070=CARTESIAN_POINT ( 'NONE',  ( 5.228794157972393997, -0.4992892829921782849, -35.69999999999999574 ) ) ;
#14075=CARTESIAN_POINT ( 'NONE',  ( 1.387648159808044790, -4.113210426322153168, -14.76414732020000287 ) ) ;
#14147=CARTESIAN_POINT ( 'NONE',  ( 3.530284718056032833, 5.524446756132658898, -4.600967428500004175 ) ) ;
#14151=CARTESIAN_POINT ( 'NONE',  ( 1.387648159808060999, -4.113210426322157609, -15.26414732020000464 ) ) ;
#14180=CARTESIAN_POINT ( 'NONE',  ( 1.112302519808859858, 4.726259607321323664, -35.70000000000000284 ) ) ;
#14188=CARTESIAN_POINT ( 'NONE',  ( -5.082228009654736312, -3.365126390422853220, -7.489929326000003940 ) ) ;
#14189=CARTESIAN_POINT ( 'NONE',  ( 1.566980368899936193, 4.067530462867746444, -25.59462237480000724 ) ) ;
#14194=CARTESIAN_POINT ( 'NONE',  ( -2.322678811625143780, -3.635533071076384015, -21.70891267860000795 ) ) ;
#14225=CARTESIAN_POINT ( 'NONE',  ( 2.946576500976501478, 4.280162264036399655, -16.21259163649999735 ) ) ;
#14305=CARTESIAN_POINT ( 'NONE',  ( -3.630162863991669209, -2.403661707492378508, -6.889929326000000742 ) ) ;
#14312=CARTESIAN_POINT ( 'NONE',  ( -4.448701673712585070, 0.6187532242676665462, -19.25159460730001371 ) ) ;
#14327=ORIENTED_EDGE ( 'NONE', *, *, #6199, .T. ) ;
#14345=CARTESIAN_POINT ( 'NONE',  ( 0.9773263286493246715, 4.731305334447203137, -35.69999999999999574 ) ) ;
#14352=CARTESIAN_POINT ( 'NONE',  ( -4.338779899226326009, -4.343559731693466652, -9.813991631000003935 ) ) ;
#14353=CARTESIAN_POINT ( 'NONE',  ( 5.307277461537168506, -2.951504967840870464, -26.93037294500000201 ) ) ;
#14361=CARTESIAN_POINT ( 'NONE',  ( -2.183849900456023896, 3.899926742306373928, -16.67761783620000315 ) ) ;
#14383=CARTESIAN_POINT ( 'NONE',  ( 3.078268752310275858, -3.892570190047870415, -0.6999653576749226280 ) ) ;
#14386=CARTESIAN_POINT ( 'NONE',  ( 4.190083271568243894, -3.954132654168471817, -18.03565260999999964 ) ) ;
#14411=CARTESIAN_POINT ( 'NONE',  ( -1.611722395286938170, -6.291674585240492057, -28.14882611459999850 ) ) ;
#14424=CARTESIAN_POINT ( 'NONE',  ( 3.540874049123775791, -2.351920722568056732, -35.09901165280005841 ) ) ;
#14459=CARTESIAN_POINT ( 'NONE',  ( 5.763395275750641922, -2.111988417859953504, -5.236105321699997539 ) ) ;
#14464=CARTESIAN_POINT ( 'NONE',  ( -2.879958020441473199, 3.829670441245457191, -20.56814294429999990 ) ) ;
#14478=CARTESIAN_POINT ( 'NONE',  ( 5.097421258188004067, 0.5103876169533114737, -30.56866556700000359 ) ) ;
#14496=CARTESIAN_POINT ( 'NONE',  ( 0.8905567152654183527, 4.062885351561556391, -35.69999999999999574 ) ) ;
#14502=CARTESIAN_POINT ( 'NONE',  ( -4.484282906631563925, 1.269983465873031347, -7.810827254900003069 ) ) ;
#14503=CARTESIAN_POINT ( 'NONE',  ( -4.781258647701263520, -0.007971864669480827059, -27.23106466010000304 ) ) ;
#14510=CARTESIAN_POINT ( 'NONE',  ( 1.265035515811502309, -4.453021097817297047, -21.29535708919999593 ) ) ;
#14537=CARTESIAN_POINT ( 'NONE',  ( 3.543796088487663809, -3.315250500659660648, -0.6997944144658480026 ) ) ;
#14542=CARTESIAN_POINT ( 'NONE',  ( 2.326244606069574505, 3.379075471592551949, -17.21259163650000446 ) ) ;
#14568=CARTESIAN_POINT ( 'NONE',  ( -4.555585884337687297, -4.059738318096004939, -24.84101932450000305 ) ) ;
#14613=CARTESIAN_POINT ( 'NONE',  ( -4.273751495587445604, 4.364932658710685587, -4.568732180600005854 ) ) ;
#14618=CARTESIAN_POINT ( 'NONE',  ( -3.664565019602479268, -2.682238183793479447, -19.81004627010000618 ) ) ;
#14632=CARTESIAN_POINT ( 'NONE',  ( 6.487627055914963137, 0.6495842397260740420, -29.63116556699998938 ) ) ;
#14649=CARTESIAN_POINT ( 'NONE',  ( 0.3116452112896634929, 4.617848473969027090, -35.69999999999999574 ) ) ;
#14655=CARTESIAN_POINT ( 'NONE',  ( -2.564224011386423641, 5.541743391105337757, -8.331725184300003306 ) ) ;
#14656=CARTESIAN_POINT ( 'NONE',  ( -5.430430790592723156, -2.746024268427175841, -27.96472909260000606 ) ) ;
#14663=CARTESIAN_POINT ( 'NONE',  ( -2.227024806490486508, -3.476280271252723431, -18.70544088819999118 ) ) ;
#14691=CARTESIAN_POINT ( 'NONE',  ( 5.782996427689181651, 1.709881257618839356, -16.94190840230000461 ) ) ;
#14717=CARTESIAN_POINT ( 'NONE',  ( 1.566980368899936193, 4.067530462867746444, -26.59462237480001079 ) ) ;
#14734=CARTESIAN_POINT ( 'NONE',  ( 3.486867635905563034, -2.515642288303716168, -0.6999999999999992895 ) ) ;
#14762=CARTESIAN_POINT ( 'NONE',  ( 6.034652528523337445, 2.501332855249893683, -10.89261350020000130 ) ) ;
#14767=CARTESIAN_POINT ( 'NONE',  ( 4.129834804009608007, 5.047645050193429128, -20.25622222230000347 ) ) ;
#14784=CARTESIAN_POINT ( 'NONE',  ( 2.499950477468926291, 3.566222500441432075, -29.21106724380000230 ) ) ;
#14800=CARTESIAN_POINT ( 'NONE',  ( 1.155622926759880986, 3.934465103449412915, -35.69999999999999574 ) ) ;
#14809=CARTESIAN_POINT ( 'NONE',  ( -4.932711197237716227, 1.396981812416056457, -8.248327254899997740 ) ) ;
#14810=CARTESIAN_POINT ( 'NONE',  ( 2.749945525234485988, 3.922844750473964748, -28.27356724379999875 ) ) ;
#14816=CARTESIAN_POINT ( 'NONE',  ( -4.363437395929419260, 0.1294788321584625090, -13.18304957890000573 ) ) ;
#14853=CARTESIAN_POINT ( 'NONE',  ( 0.5830502407437251344, -4.723335260236232180, -17.43304674910000429 ) ) ;
#14878=CARTESIAN_POINT ( 'NONE',  ( 4.807767551039155762, 1.738376938488521040, -27.44999766020000465 ) ) ;
#14894=CARTESIAN_POINT ( 'NONE',  ( 3.075842487415840765, -2.801017835266844891, -0.6999999999999992895 ) ) ;
#14907=EDGE_LOOP ( 'NONE', ( #5379, #5139 ) ) ;
#14919=CARTESIAN_POINT ( 'NONE',  ( 4.880902371519058036, -3.592936783560450653, -8.372776792900001652 ) ) ;
#14924=CARTESIAN_POINT ( 'NONE',  ( -5.635022120040177995, 0.7837540840564873879, -20.25159460730000305 ) ) ;
#14937=CARTESIAN_POINT ( 'NONE',  ( -5.864216825196034932, 1.669623860970033347, -31.30158078969999380 ) ) ;
#14956=CARTESIAN_POINT ( 'NONE',  ( 0.5877407897813119453, -4.297347728519514298, 0.1268759519999947127 ) ) ;
#14959=CARTESIAN_POINT ( 'NONE',  ( -2.014747437493234816, 4.354226950121528716, -8.669225184300003662 ) ) ;
#14960=CARTESIAN_POINT ( 'NONE',  ( 1.844957972340690588, -5.198917526286033208, -29.25632401680000427 ) ) ;
#14998=CARTESIAN_POINT ( 'NONE',  ( 4.324151835433248436, -2.064520475586355985, -19.94430150030000348 ) ) ;
#15026=CARTESIAN_POINT ( 'NONE',  ( -0.6320852424383932577, 6.069672320066970883, -25.88903409330001182 ) ) ;
#15046=CARTESIAN_POINT ( 'NONE',  ( 0.7846218181574846628, -3.768377790190448717, -0.6999999999999992895 ) ) ;
#15074=CARTESIAN_POINT ( 'NONE',  ( -5.151963982244392781, -3.152247574024123811, -22.50799200640000919 ) ) ;
#15091=CARTESIAN_POINT ( 'NONE',  ( -2.705882613314523955, 5.963358562559473164, -31.72635571290000200 ) ) ;
#15105=CARTESIAN_POINT ( 'NONE',  ( 2.716715618103660024, 4.270696308027718047, -35.69999999999998863 ) ) ;
#15107=CARTESIAN_POINT ( 'NONE',  ( -4.345470169637781765, 2.035989658359887766, -0.6999999999999991784 ) ) ;
#15111=CARTESIAN_POINT ( 'NONE',  ( 2.536150288113629081, -3.576595042060319862, -12.62388893670000023 ) ) ;
#15112=CARTESIAN_POINT ( 'NONE',  ( -4.274658871253808279, -0.8336587121505223408, -30.59652066319999975 ) ) ;
#15117=CARTESIAN_POINT ( 'NONE',  ( 2.022420680230021972, -3.847796821814266632, -33.20721934060000535 ) ) ;
#15146=CARTESIAN_POINT ( 'NONE',  ( 2.949882002856674124, 3.605460750137338799, -20.25622222230000347 ) ) ;
#15188=CARTESIAN_POINT ( 'NONE',  ( -1.804682441769323464, -3.297106965646906751, -0.6999999999999991784 ) ) ;
#15222=CARTESIAN_POINT ( 'NONE',  ( -5.151963982244392781, -3.152247574024123811, -21.90799200640000777 ) ) ;
#15235=CARTESIAN_POINT ( 'NONE',  ( -3.850850186879767545, -3.402327863231305205, -34.77197003409999354 ) ) ;
#15249=CARTESIAN_POINT ( 'NONE',  ( 3.835128050359830176, 3.444395927274146452, -35.69999999999999574 ) ) ;
#15254=CARTESIAN_POINT ( 'NONE',  ( -3.893462112830481825, 1.255681637813407248, -0.6999999999999992895 ) ) ;
#15255=CARTESIAN_POINT ( 'NONE',  ( 4.373195337096347224, -2.904765488536225515, 0.04124526979999709742 ) ) ;
#15259=CARTESIAN_POINT ( 'NONE',  ( -1.657635364023947400, -6.345118362804027079, -12.55022317840000312 ) ) ;
#15260=CARTESIAN_POINT ( 'NONE',  ( 1.602200344400662058, -4.514849430718075318, -29.31882401680000072 ) ) ;
#15269=VECTOR ( 'NONE', #19365, 1000.000000000000114 ) ;
#15301=CARTESIAN_POINT ( 'NONE',  ( 2.914708617673698932, -3.631324690002109445, -3.105321867099997135 ) ) ;
#15302=CARTESIAN_POINT ( 'NONE',  ( 5.503465972402116435, -2.627571514392686769, -20.28180150030001272 ) ) ;
#15343=CARTESIAN_POINT ( 'NONE',  ( 3.162069896769252431, -2.100311282821142100, -35.69999999999999574 ) ) ;
#15347=CARTESIAN_POINT ( 'NONE',  ( 0.2775905903481815651, -3.807106439044698920, -0.6999999999999991784 ) ) ;
#15378=CARTESIAN_POINT ( 'NONE',  ( 3.710789578725085303, 2.835545959904683500, -23.86727430110000370 ) ) ;
#15392=CARTESIAN_POINT ( 'NONE',  ( 1.882647771056455976, 3.960165260869605408, -32.15113063600000487 ) ) ;
#15408=CARTESIAN_POINT ( 'NONE',  ( -4.804319815618600664, 1.211543436087829217, -0.6999999999999994005 ) ) ;
#15413=CARTESIAN_POINT ( 'NONE',  ( 5.466312515054250198, -2.792605348973308477, -11.91474735220000092 ) ) ;
#15414=CARTESIAN_POINT ( 'NONE',  ( 4.437687981975763307, 3.340062028235890601, -31.36032172560000930 ) ) ;
#15419=CARTESIAN_POINT ( 'NONE',  ( 3.790912472548403578, -2.108217834232220422, -26.93037294500000201 ) ) ;
#15430=VECTOR ( 'NONE', #5390, 1000.000000000000114 ) ;
#15451=CARTESIAN_POINT ( 'NONE',  ( -1.949381390262891589, -5.750991590113663676, -1.175630512700004404 ) ) ;
#15452=CARTESIAN_POINT ( 'NONE',  ( 4.354753084053718304, 0.1085053810021633369, -20.17661200060000581 ) ) ;
#15466=CARTESIAN_POINT ( 'NONE',  ( 5.763395275833943288, -2.111988417915284355, -5.836105321700000736 ) ) ;
#15489=CARTESIAN_POINT ( 'NONE',  ( -5.857861475075242019, -1.837656413297739766, -9.423230889000002719 ) ) ;
#15506=SHAPE_REPRESENTATION_RELATIONSHIP ( 'NONE' , 'NONE' ,  #16405, #25297 ) ;
#15528=CARTESIAN_POINT ( 'NONE',  ( 3.710789578725101734, 2.835545959904678170, -23.36727430110000014 ) ) ;
#15541=CARTESIAN_POINT ( 'NONE',  ( 2.022420680230010870, -3.847796821814265300, -33.70721934059999825 ) ) ;
#15546=ORIENTED_EDGE ( 'NONE', *, *, #7989, .F. ) ;
#15554=CARTESIAN_POINT ( 'NONE',  ( -5.016375772021067547, 0.4838088423305476060, -0.6999999999999992895 ) ) ;
#15555=CARTESIAN_POINT ( 'NONE',  ( 1.537204335059164872, 5.727607561491170785, -1.053410702900002160 ) ) ;
#15560=CARTESIAN_POINT ( 'NONE',  ( 6.034652528523337445, 2.501332855249893683, -12.09261350020000236 ) ) ;
#15561=CARTESIAN_POINT ( 'NONE',  ( -1.932773295258156887, 4.259541830411037289, -31.72635571290000200 ) ) ;
#15566=CARTESIAN_POINT ( 'NONE',  ( 0.07512830594656044747, -4.346272141329931671, -33.41110030499999795 ) ) ;
#15602=CARTESIAN_POINT ( 'NONE',  ( -4.757675747652303500, -1.918655839533711660, -1.934697434500002755 ) ) ;
#15603=CARTESIAN_POINT ( 'NONE',  ( -0.7560282158644051620, 4.289996408053716515, -19.33583244400000822 ) ) ;
#15619=CARTESIAN_POINT ( 'NONE',  ( 0.2392016894930265591, 6.101552847015987879, -7.937690181100006903 ) ) ;
#15639=CARTESIAN_POINT ( 'NONE',  ( -0.8069922590487529357, 5.436669193145879042, -9.867720916600005054 ) ) ;
#15694=CARTESIAN_POINT ( 'NONE',  ( 0.08264113651937701754, -4.780899355463231970, -34.34860030499999795 ) ) ;
#15711=CARTESIAN_POINT ( 'NONE',  ( -6.055223678858003389, -2.441925613954294860, -0.9971974345000036433 ) ) ;
#15715=CARTESIAN_POINT ( 'NONE',  ( -4.101794773660127902, 5.071170285176791914, -13.60352819870000474 ) ) ;
#15716=CARTESIAN_POINT ( 'NONE',  ( 4.051823674760414384, -0.6775361292690335047, -35.24517599850000238 ) ) ;
#15737=CARTESIAN_POINT ( 'NONE',  ( 1.422193333878468691, -4.930531469442030357, -0.7000165122823585051 ) ) ;
#15750=CARTESIAN_POINT ( 'NONE',  ( 3.421672250023957140, 1.629039945493292896, -35.69999999999999574 ) ) ;
#15760=CARTESIAN_POINT ( 'NONE',  ( 2.816286225276055433, -4.345042730952153320, -1.165939388299997770 ) ) ;
#15761=CARTESIAN_POINT ( 'NONE',  ( 4.081868536579633222, 3.119100555900671257, -22.42977430109999659 ) ) ;
#15799=CARTESIAN_POINT ( 'NONE',  ( 4.334836395473461224, -2.879286697580460519, -35.69999999999999574 ) ) ;
#15803=CARTESIAN_POINT ( 'NONE',  ( -4.338779899226326009, -4.343559731693466652, -9.813991631000003935 ) ) ;
#15868=CARTESIAN_POINT ( 'NONE',  ( 4.904813032679735230, 3.691647504909488564, -32.96032172560001072 ) ) ;
#15883=CARTESIAN_POINT ( 'NONE',  ( -3.175770273322759518, 4.553269643686719270, -0.6276513541000027230 ) ) ;
#15886=CARTESIAN_POINT ( 'NONE',  ( 1.757687669117797835, -5.210066540036287996, -16.26414732020001352 ) ) ;
#15887=CARTESIAN_POINT ( 'NONE',  ( -3.500772897184941446, -3.093025330206539802, -33.33447003410001486 ) ) ;
#15919=CARTESIAN_POINT ( 'NONE',  ( 1.334940606749785319, 4.973974987606708531, -2.990910702900007934 ) ) ;
#15920=CARTESIAN_POINT ( 'NONE',  ( 3.375516224911109031, -2.766870103071180420, -23.49674734059999892 ) ) ;
#15946=( BOUNDED_CURVE ( )  B_SPLINE_CURVE ( 5, ( #13413, #25391, #18289, #10595, #30100, #22707, #6178, #8211, #8528, #1474, #6021, #853, #18129, #8685, #29940, #25545, #29781, #17964, #15466, #3981, #20038, #1151, #27576, #25069, #15619, #25226, #11065, #5709, #27731, #20662, #3827, #17659, #3656, #13578, #10743, #23029, #30257, #12953, #22563, #27272, #29635, #20344, #8368, #27422, #17814, #5860, #13253, #3502, #22871, #1313, #27896, #10908, #1007, #20500, #8064, #6340, #10444, #20189, #16700, #31037, #18451, #9475, #9156, #11378, #23184, #18759, #21440, #7115, #18917, #11218, #1627, #6646, #23345, #6807, #30428, #19076, #4453, #28360, #20974, #28049, #1788, #30886, #2092, #6492, #26317, #28671, #16093, #28516, #8845, #14053, #16403, #16244, #4763, #25861, #26162, #4299, #18607, #20818, #13894, #25705, #23657, #6962, #26010, #4135, #21133, #30580, #13734, #9006 ),
 .UNSPECIFIED., .F., .T. ) 
 B_SPLINE_CURVE_WITH_KNOTS ( ( 6, 3, 3, 3, 3, 3, 3, 3, 3, 3, 3, 3, 3, 3, 3, 3, 3, 3, 3, 3, 3, 3, 3, 3, 3, 3, 3, 3, 3, 3, 3, 3, 3, 3, 3, 6 ),
 ( 8.193316113699999903, 11.38862009670000042, 23.17260734259999921, 34.79167593860000096, 46.25425528950000142, 57.87229377410000097, 69.67120816000000616, 81.20502170430000888, 92.80704244430000927, 104.1208912060000102, 115.9269080290000034, 127.3307717769999954, 139.1306782750000082, 150.7654282180000109, 162.2434640489999822, 173.6637378899999931, 185.2020570420000070, 194.1769840820000184, 203.3038760180000111, 212.5853790139999830, 224.1393301890000203, 235.6932813649999900, 246.8715721780000081, 258.4996770380000157, 270.1277818960000445, 281.7035649139999691, 293.2822232819999613, 304.6732510989999696, 316.1434960830000023, 327.6894369340000139, 339.2353777880000507, 350.7813186390000055, 362.5843219139999860, 374.0573691040000313, 385.8560256169999434, 394.7457478480000077 ),
 .UNSPECIFIED. ) 
 CURVE ( )  GEOMETRIC_REPRESENTATION_ITEM ( )  RATIONAL_B_SPLINE_CURVE ( ( 0.2500000000000000000, 0.2500000000000000000, 0.2500000000000000000, 0.2500000000000000000, 0.2500000000000000000, 0.2500000000000000000, 0.2500000000000000000, 0.2500000000000000000, 0.2500000000000000000, 0.2500000000000000000, 0.2500000000000000000, 0.2500000000000000000, 0.2500000000000000000, 0.2500000000000000000, 0.2500000000000000000, 0.2500000000000000000, 0.2500000000000000000, 0.2500000000000000000, 0.2500000000000000000, 0.2500000000000000000, 0.2500000000000000000, 0.2500000000000000000, 0.2500000000000000000, 0.2500000000000000000, 0.2500000000000000000, 0.2500000000000000000, 0.2500000000000000000, 0.2500000000000000000, 0.2500000000000000000, 0.2500000000000000000, 0.2500000000000000000, 0.2500000000000000000, 0.2500000000000000000, 0.2500000000000000000, 0.2500000000000000000, 0.2500000000000000000, 0.2500000000000000000, 0.2500000000000000000, 0.2500000000000000000, 0.2500000000000000000, 0.2500000000000000000, 0.2500000000000000000, 0.2500000000000000000, 0.2500000000000000000, 0.2500000000000000000, 0.2500000000000000000, 0.2500000000000000000, 0.2500000000000000000, 0.2500000000000000000, 0.2500000000000000000, 0.2500000000000000000, 0.2500000000000000000, 0.2500000000000000000, 0.2500000000000000000, 0.2500000000000000000, 0.2500000000000000000, 0.2500000000000000000, 0.2500000000000000000, 0.2500000000000000000, 0.2500000000000000000, 0.2500000000000000000, 0.2500000000000000000, 0.2500000000000000000, 0.2500000000000000000, 0.2500000000000000000, 0.2500000000000000000, 0.2500000000000000000, 0.2500000000000000000, 0.2500000000000000000, 0.2500000000000000000, 0.2500000000000000000, 0.2500000000000000000, 0.2500000000000000000, 0.2500000000000000000, 0.2500000000000000000, 0.2500000000000000000, 0.2500000000000000000, 0.2500000000000000000, 0.2500000000000000000, 0.2500000000000000000, 0.2500000000000000000, 0.2500000000000000000, 0.2500000000000000000, 0.2500000000000000000, 0.2500000000000000000, 0.2500000000000000000, 0.2500000000000000000, 0.2500000000000000000, 0.2500000000000000000, 0.2500000000000000000, 0.2500000000000000000, 0.2500000000000000000, 0.2500000000000000000, 0.2500000000000000000, 0.2500000000000000000, 0.2500000000000000000, 0.2500000000000000000, 0.2500000000000000000, 0.2500000000000000000, 0.2500000000000000000, 0.2500000000000000000, 0.2500000000000000000, 0.2500000000000000000, 0.2500000000000000000, 0.2500000000000000000, 0.2500000000000000000, 0.2500000000000000000, 0.2500000000000000000 ) ) 
 REPRESENTATION_ITEM ( '' )  );
#15957=CARTESIAN_POINT ( 'NONE',  ( 4.586950623478608158, -2.526155056066153648, -35.69999999999999574 ) ) ;
#15960=CARTESIAN_POINT ( 'NONE',  ( 1.086829820489895848, 5.988658659452708477, -14.02400681850000197 ) ) ;
#16033=CARTESIAN_POINT ( 'NONE',  ( -2.507187057889202819, 3.594686560818132204, -1.127651354099999725 ) ) ;
#16037=CARTESIAN_POINT ( 'NONE',  ( 4.630235822890134578, 0.3309221515414850767, -14.64454535870000207 ) ) ;
#16050=DIRECTION ( 'NONE',  ( 0.000000000000000000, 0.000000000000000000, 1.000000000000000000 ) ) ;
#16076=CARTESIAN_POINT ( 'NONE',  ( -2.624260084387257219, -3.463915187244964056, -3.728945369300004753 ) ) ;
#16077=CARTESIAN_POINT ( 'NONE',  ( -4.555585884337687297, -4.059738318096004939, -24.24101932449999808 ) ) ;
#16093=CARTESIAN_POINT ( 'NONE',  ( 0.8594151385421661127, 6.036396974313712249, -29.00600711719999936 ) ) ;
#16111=CARTESIAN_POINT ( 'NONE',  ( 4.969670261926683708, -1.740894218915336911, -35.69999999999999574 ) ) ;
#16114=CARTESIAN_POINT ( 'NONE',  ( -3.222838750790782303, 3.984490938364168233, -12.66602819870000296 ) ) ;
#16170=CARTESIAN_POINT ( 'NONE',  ( 4.618385388201741826, 1.362661324479865099, -36.46909726779999517 ) ) ;
#16187=CARTESIAN_POINT ( 'NONE',  ( 5.523879335194060936, -0.1907134851046367874, -1.685409721200002764 ) ) ;
#16191=CARTESIAN_POINT ( 'NONE',  ( -5.990533020055879732, -1.129328118392731950, -16.09949426530000238 ) ) ;
#16192=CARTESIAN_POINT ( 'NONE',  ( 5.318140750231298064, 1.569125161471404573, -34.53159726779999517 ) ) ;
#16210=CARTESIAN_POINT ( 'NONE',  ( 0.09454741856676797396, -5.198049559341232140, -0.7000607835638984477 ) ) ;
#16222=CARTESIAN_POINT ( 'NONE',  ( 3.650208047081187512, 0.9579503420338048025, -35.69999999999999574 ) ) ;
#16228=CARTESIAN_POINT ( 'NONE',  ( -1.295942751353782674, 4.166547562507306957, -5.274955258300003891 ) ) ;
#16229=CARTESIAN_POINT ( 'NONE',  ( -3.253989917302557267, -2.899813084402114161, -24.34101932450000305 ) ) ;
#16244=CARTESIAN_POINT ( 'NONE',  ( -3.231711866632715147, -5.662799918003592836, -30.67642233980000199 ) ) ;
#16257=AXIS2_PLACEMENT_3D ( 'NONE', #9114, #13689, #16050 ) ;
#16265=CARTESIAN_POINT ( 'NONE',  ( 3.665953941183818010, 4.858601989977915814, -14.22796858840000311 ) ) ;
#16317=FACE_OUTER_BOUND ( 'NONE', #20979, .T. ) ;
#16320=CARTESIAN_POINT ( 'NONE',  ( 0.1708583496781539146, 4.358252033550397364, -7.437690181100002462 ) ) ;
#16344=CARTESIAN_POINT ( 'NONE',  ( 4.781918068392163157, 0.6270375808061986467, -4.689479598399999283 ) ) ;
#16348=CARTESIAN_POINT ( 'NONE',  ( -5.990533020055879732, -1.129328118392731950, -16.69949426530000025 ) ) ;
#16349=CARTESIAN_POINT ( 'NONE',  ( 0.1051796283266584475, -6.084780997910130829, -32.81110030499999652 ) ) ;
#16356=PLANE ( 'NONE',  #16257 ) ;
#16385=CARTESIAN_POINT ( 'NONE',  ( 2.246931792404676997, -6.149078805876593279, -6.260585232200001293 ) ) ;
#16386=CARTESIAN_POINT ( 'NONE',  ( -0.5718866478877175918, 5.491608289559616551, -24.88903409330000116 ) ) ;
#16403=CARTESIAN_POINT ( 'NONE',  ( 2.039164074698236906, -5.746172002732055084, -30.25632401680000783 ) ) ;
#16405=SHAPE_REPRESENTATION ( 'Drive Spring', ( #17722 ), #11232 ) ;
#16421=CARTESIAN_POINT ( 'NONE',  ( 5.239171942370466795, -0.3666422309894779019, -35.69999999999999574 ) ) ;
#16424=CARTESIAN_POINT ( 'NONE',  ( -3.711147652395973662, 4.588201686596787177, -12.60352819870001184 ) ) ;
#16495=CARTESIAN_POINT ( 'NONE',  ( 0.1879441846346346090, 4.794077236920960772, -7.000190181100000686 ) ) ;
#16500=CARTESIAN_POINT ( 'NONE',  ( -2.345194346458620682, -4.011532291445383258, -15.68182079290000175 ) ) ;
#16532=CARTESIAN_POINT ( 'NONE',  ( 0.2440535278923537388, 4.404678305699071927, -35.69999999999998863 ) ) ;
#16539=CARTESIAN_POINT ( 'NONE',  ( -2.150134890876696847, -3.785840986416655340, -7.185065142700006291 ) ) ;
#16540=CARTESIAN_POINT ( 'NONE',  ( 1.984841800599668638, 5.152205253018144582, -25.09462237480000368 ) ) ;
#16545=CARTESIAN_POINT ( 'NONE',  ( 1.387648159808060999, -4.113210426322157609, -15.26414732020000464 ) ) ;
#16572=CARTESIAN_POINT ( 'NONE',  ( 3.534785842709389669, -3.329260007524329712, -0.6997833233010605225 ) ) ;
#16576=CARTESIAN_POINT ( 'NONE',  ( -2.345194346458620682, -4.011532291445383258, -15.68182079290000175 ) ) ;
#16647=CARTESIAN_POINT ( 'NONE',  ( -3.866727543631055308, 3.949224786475222349, -3.568732180600000525 ) ) ;
#16651=CARTESIAN_POINT ( 'NONE',  ( 5.503465972402116435, -2.627571514392686769, -20.88180150029999993 ) ) ;
#16681=CARTESIAN_POINT ( 'NONE',  ( 0.7667278788745763851, 4.120231142481624254, -35.70000000000000284 ) ) ;
#16687=CARTESIAN_POINT ( 'NONE',  ( -3.630162863991669209, -2.403661707492378508, -6.889929326000000742 ) ) ;
#16688=CARTESIAN_POINT ( 'NONE',  ( 2.193772516446764076, 5.694542648089183423, -26.09462237480000724 ) ) ;
#16693=CARTESIAN_POINT ( 'NONE',  ( 0.7763070146520680836, 4.277613328189620923, -14.02400681850000197 ) ) ;
#16700=CARTESIAN_POINT ( 'NONE',  ( -6.228182343209494043, 0.8662545139425728014, -19.25159460730001371 ) ) ;
#16721=CARTESIAN_POINT ( 'NONE',  ( 2.992916622598568388, -2.824380467281232487, -18.03565260999999964 ) ) ;
#16753=CARTESIAN_POINT ( 'NONE',  ( 1.723678405763061194, 4.474283509182772178, -27.03212237480000013 ) ) ;
#16765=CARTESIAN_POINT ( 'NONE',  ( 3.162069896769252875, -2.100311282821142100, -35.69999999999999574 ) ) ;
#16802=CARTESIAN_POINT ( 'NONE',  ( -1.641527485091622385, 5.277626912542655369, -3.774955258300002114 ) ) ;
#16807=CARTESIAN_POINT ( 'NONE',  ( -6.228182343209494043, 0.8662545139425728014, -19.85159460730000092 ) ) ;
#16843=CARTESIAN_POINT ( 'NONE',  ( 0.2815792077273640004, 4.370109598415317542, -35.69999999999998863 ) ) ;
#16849=CARTESIAN_POINT ( 'NONE',  ( -6.277996069133942925, 1.777976852108807737, -7.910827254899999161 ) ) ;
#16850=CARTESIAN_POINT ( 'NONE',  ( 4.170003719754086013, -2.319039617606510006, -25.99287294500000201 ) ) ;
#16856=CARTESIAN_POINT ( 'NONE',  ( -2.345194346458620682, -4.011532291445383258, -15.68182079290000175 ) ) ;
#16881=CARTESIAN_POINT ( 'NONE',  ( 3.843630909669756957, -2.553018000905745044, -0.6999999999999992895 ) ) ;
#16885=CARTESIAN_POINT ( 'NONE',  ( 1.403799475828179766, 5.569137675590418723, -16.45080441500000745 ) ) ;
#16909=CARTESIAN_POINT ( 'NONE',  ( 5.307277461537168506, -2.951504967840870464, -27.53037294499999277 ) ) ;
#16959=CARTESIAN_POINT ( 'NONE',  ( -4.598206294437411579, -3.044638162784917945, -5.889929326000000742 ) ) ;
#16964=CARTESIAN_POINT ( 'NONE',  ( 3.800013225884302237, -1.579422177728474708, -17.87122516810000405 ) ) ;
#16980=CARTESIAN_POINT ( 'NONE',  ( 6.487627055914963137, 0.6495842397260740420, -30.23116556699999435 ) ) ;
#16996=CARTESIAN_POINT ( 'NONE',  ( 0.7245117006341926791, 4.718262249271010234, -35.69999999999999574 ) ) ;
#17005=CARTESIAN_POINT ( 'NONE',  ( 3.486358836775539594, -2.566383416802844319, -8.972776792899997744 ) ) ;
#17006=CARTESIAN_POINT ( 'NONE',  ( -4.346598770676703083, -0.007247149673123010061, -28.16856466009999593 ) ) ;
#17013=CARTESIAN_POINT ( 'NONE',  ( -0.6370991518874352666, 4.292107257743940529, -10.86772091660000150 ) ) ;
#17042=CARTESIAN_POINT ( 'NONE',  ( 3.791027721911684800, -3.577548591872723449, -17.03565261000001385 ) ) ;
#17067=CARTESIAN_POINT ( 'NONE',  ( -3.253989917302557267, -2.899813084402114161, -25.34101932449999595 ) ) ;
#17112=CARTESIAN_POINT ( 'NONE',  ( 3.904508939291361003, -1.994718106397497914, -11.91474735220000092 ) ) ;
#17118=CARTESIAN_POINT ( 'NONE',  ( -0.8316310374238428116, 4.718996048841939128, -20.77333244400000822 ) ) ;
#17131=CARTESIAN_POINT ( 'NONE',  ( -3.231711866632715147, -5.662799918003592836, -30.67642233980000199 ) ) ;
#17144=CARTESIAN_POINT ( 'NONE',  ( 0.3318591986118693549, 4.627280206481456659, -35.69999999999999574 ) ) ;
#17147=CARTESIAN_POINT ( 'NONE',  ( -2.017871889752692383, -3.161030873707806332, -0.6999999999999992895 ) ) ;
#17151=CARTESIAN_POINT ( 'NONE',  ( 0.4590887144193210312, -5.884162454197269909, -10.39338421180000438 ) ) ;
#17152=CARTESIAN_POINT ( 'NONE',  ( -4.273414424137721213, 4.913340199448848367, -27.98728588870000422 ) ) ;
#17158=CARTESIAN_POINT ( 'NONE',  ( 0.5300456733980246637, -4.293941145674104121, -18.37054674910000429 ) ) ;
#17191=CARTESIAN_POINT ( 'NONE',  ( 3.800013225884302237, -1.579422177728474708, -17.87122516810000405 ) ) ;
#17216=CARTESIAN_POINT ( 'NONE',  ( -5.367600138795724618, 3.713494282866228069, -25.46779765530001072 ) ) ;
#17222=FILL_AREA_STYLE ('',( #3519 ) ) ;
#17250=B_SPLINE_CURVE_WITH_KNOTS ( 'NONE', 5,
 ( #15799, #15957, #25563, #16111, #18776, #18934, #14070, #16421, #21460 ),
 .UNSPECIFIED., .F., .F.,
 ( 6, 3, 6 ),
 ( 0.000000000000000000, 3.075806851740000347, 4.017655677589999641 ),
 .UNSPECIFIED. ) ;
#17254=EDGE_CURVE ( 'NONE', #29606, #18476, #9701, .T. ) ;
#17265=CARTESIAN_POINT ( 'NONE',  ( 4.262818619062177738, -0.7545854518158033875, -8.271482634700015879 ) ) ;
#17271=CARTESIAN_POINT ( 'NONE',  ( -2.820898088245517688, -4.403288343584588205, -19.70544088820000184 ) ) ;
#17288=CARTESIAN_POINT ( 'NONE',  ( -5.505691776210679400, -0.009179722898969058451, -29.16856466010000304 ) ) ;
#17302=CARTESIAN_POINT ( 'NONE',  ( 1.629408644310613052, 4.659406692139858919, -35.70000000000000284 ) ) ;
#17304=CARTESIAN_POINT ( 'NONE',  ( -3.679671488369449683, -1.085031249664836439, -0.6999999999999991784 ) ) ;
#17311=CARTESIAN_POINT ( 'NONE',  ( -4.345037505360560992, 2.733239894040710105, -11.38297590280000016 ) ) ;
#17312=CARTESIAN_POINT ( 'NONE',  ( -2.705882613314523955, 5.963358562559473164, -31.72635571290000200 ) ) ;
#17350=CARTESIAN_POINT ( 'NONE',  ( -2.183849900456023896, 3.899926742306373928, -16.67761783620000315 ) ) ;
#17372=CARTESIAN_POINT ( 'NONE',  ( 2.450607853129171954, -3.579122932049592976, -27.63292313650000054 ) ) ;
#17394=CARTESIAN_POINT ( 'NONE',  ( 2.129400989689198997, -3.370417416381545905, -0.6999999999999992895 ) ) ;
#17418=CARTESIAN_POINT ( 'NONE',  ( -3.409041349409528632, -3.412796932024714014, -8.876491631000003935 ) ) ;
#17419=ADVANCED_FACE ( 'NONE', ( #30759 ), #26498, .F. ) ;
#17425=CARTESIAN_POINT ( 'NONE',  ( 0.2309929099465271585, 4.358477053493584386, -22.94418644579999977 ) ) ;
#17439=CARTESIAN_POINT ( 'NONE',  ( 4.634019325638258024, 0.4639887426745141208, -30.13116556700000714 ) ) ;
#17456=CARTESIAN_POINT ( 'NONE',  ( -5.082955080895779965, -0.02874842474374714185, -0.6999999999999992895 ) ) ;
#17460=CARTESIAN_POINT ( 'NONE',  ( 2.789765316938662476, -3.934254546267435426, -13.06138893670000023 ) ) ;
#17461=CARTESIAN_POINT ( 'NONE',  ( 3.999349870826697018, -3.799712354642017509, -29.05126389020000133 ) ) ;
#17468=CARTESIAN_POINT ( 'NONE',  ( -4.215937884789293655, -1.105999120962562809, -25.04656121680000425 ) ) ;
#17502=CARTESIAN_POINT ( 'NONE',  ( -3.331422745097512017, -2.438398348906446689, -18.87254627010000263 ) ) ;
#17543=CARTESIAN_POINT ( 'NONE',  ( -0.3657832974528221759, -3.774695518882208667, -0.6999999999999992895 ) ) ;
#17555=( NAMED_UNIT ( * ) SI_UNIT ( $, .STERADIAN. ) SOLID_ANGLE_UNIT ( ) );
#17576=CARTESIAN_POINT ( 'NONE',  ( 0.2925910193319765096, 5.520737601085913937, -23.94418644580000688 ) ) ;
#17590=CARTESIAN_POINT ( 'NONE',  ( 3.503437880490057665, 2.636891074952370850, -32.86032172560000220 ) ) ;
#17604=CARTESIAN_POINT ( 'NONE',  ( 5.245096043587340162, -0.2338077457563897399, -35.69999999999999574 ) ) ;
#17605=CARTESIAN_POINT ( 'NONE',  ( 3.746497173757565413, -0.1670055334890632737, -35.69999999999999574 ) ) ;
#17607=CARTESIAN_POINT ( 'NONE',  ( -4.088025854205739940, 2.308258268490227305, -0.6999999999999991784 ) ) ;
#17611=CARTESIAN_POINT ( 'NONE',  ( 3.316815470610420924, 4.395877990916175371, -15.22796858840000311 ) ) ;
#17612=CARTESIAN_POINT ( 'NONE',  ( 1.456545767631101107, -4.104408573385627257, -30.25632401680000783 ) ) ;
#17645=CARTESIAN_POINT ( 'NONE',  ( 3.950106903291092930, 1.853988655799142959, -2.979170051700004151 ) ) ;
#17646=CARTESIAN_POINT ( 'NONE',  ( -4.893571841047932303, 0.6806285466545627383, -18.31409460729999950 ) ) ;
#17659=CARTESIAN_POINT ( 'NONE',  ( -5.530047734074942767, 3.478668956039820959, -10.44547590279999660 ) ) ;
#17687=CARTESIAN_POINT ( 'NONE',  ( 3.258358799905588299, -2.671990297561158467, -0.6999999999999992895 ) ) ;
#17720=CARTESIAN_POINT ( 'NONE',  ( 5.195105410215491659, 3.969764343816663210, -23.36727430110000014 ) ) ;
#17722=AXIS2_PLACEMENT_3D ( 'NONE', #2627, #14015, #29203 ) ;
#17735=CARTESIAN_POINT ( 'NONE',  ( 4.556810990865948874, -1.030009251744163468, -33.28377053309998956 ) ) ;
#17747=CARTESIAN_POINT ( 'NONE',  ( 3.609060361128767713, 3.656617855560637231, -35.69999999999999574 ) ) ;
#17751=CARTESIAN_POINT ( 'NONE',  ( -3.935256165287342789, 0.8486244890569863975, -0.6999999999999994005 ) ) ;
#17752=CARTESIAN_POINT ( 'NONE',  ( 3.956700543085260424, -2.628121156294163541, 1.041245269799995876 ) ) ;
#17756=CARTESIAN_POINT ( 'NONE',  ( -1.184025259985572953, -4.532227402022651397, -12.55022317840000312 ) ) ;
#17757=CARTESIAN_POINT ( 'NONE',  ( 2.070912548172440637, 4.356181786950492629, -31.21363063600000487 ) ) ;
#17798=CARTESIAN_POINT ( 'NONE',  ( -6.055223678858003389, -2.441925613954294860, -1.597197434499999957 ) ) ;
#17799=CARTESIAN_POINT ( 'NONE',  ( -2.618143654921853969, 3.481518582925489991, -19.13064294430000345 ) ) ;
#17814=CARTESIAN_POINT ( 'NONE',  ( 4.315341029122434335, -4.279276102762477940, -15.06112212870000455 ) ) ;
#17845=CARTESIAN_POINT ( 'NONE',  ( 3.233307954802753237, -2.689733879864655286, -0.6999999999999992895 ) ) ;
#17877=CARTESIAN_POINT ( 'NONE',  ( 4.275653884846098762, -3.504702130532165505, -24.99674734060000603 ) ) ;
#17890=CARTESIAN_POINT ( 'NONE',  ( -4.339197174995634398, 0.6278332542688190854, -34.75783976330000513 ) ) ;
#17907=CARTESIAN_POINT ( 'NONE',  ( -3.928330961999677573, 0.9358211253549650888, -0.6999999999999992895 ) ) ;
#17908=CARTESIAN_POINT ( 'NONE',  ( 1.213582369797461258, 4.521795443253901148, -2.053410702900000828 ) ) ;
#17911=CARTESIAN_POINT ( 'NONE',  ( 1.708629737455300335, 5.223905898740939691, -12.07047964829999920 ) ) ;
#17912=CARTESIAN_POINT ( 'NONE',  ( 0.07512830594656044747, -4.346272141329931671, -33.41110030499999795 ) ) ;
#17917=CARTESIAN_POINT ( 'NONE',  ( 4.370697773661016861, 1.580342671372844787, -26.51249766020000109 ) ) ;
#17947=CARTESIAN_POINT ( 'NONE',  ( 0.5877407897813119453, -4.297347728519514298, -0.8731240480000050930 ) ) ;
#17948=CARTESIAN_POINT ( 'NONE',  ( -3.679974273075529823, -2.251605409995534490, -21.90799200640000777 ) ) ;
#17964=CARTESIAN_POINT ( 'NONE',  ( 6.086077541567210147, 0.7980478301550381071, -5.626979598400000171 ) ) ;
#17988=CARTESIAN_POINT ( 'NONE',  ( 5.067327387632984959, 4.072231104569050686, -8.354586407999999409 ) ) ;
#18048=CARTESIAN_POINT ( 'NONE',  ( -1.932773295258156887, 4.259541830411037289, -31.72635571290000200 ) ) ;
#18065=CARTESIAN_POINT ( 'NONE',  ( -3.891464495754538788, 2.436882555160391650, -0.6999999999999989564 ) ) ;
#18066=CARTESIAN_POINT ( 'NONE',  ( -4.921927080085812811, 2.567569881136803733, -0.4187643563000054137 ) ) ;
#18070=CARTESIAN_POINT ( 'NONE',  ( -0.8069922590487529357, 5.436669193145879042, -11.86772091660000505 ) ) ;
#18071=CARTESIAN_POINT ( 'NONE',  ( -4.339197174995634398, 0.6278332542688190854, -33.75783976330001224 ) ) ;
#18110=CARTESIAN_POINT ( 'NONE',  ( 5.530149664617865390, 2.595584118083901881, -3.079170051700004684 ) ) ;
#18111=CARTESIAN_POINT ( 'NONE',  ( 3.710789578725085303, 2.835545959904683500, -22.86727430110000014 ) ) ;
#18129=CARTESIAN_POINT ( 'NONE',  ( -3.673964118176227700, -4.849481262172373519, -3.728945369300004753 ) ) ;
#18149=CARTESIAN_POINT ( 'NONE',  ( -4.602605444716575178, -1.443872896163948205, -9.085730889000004140 ) ) ;
#18208=CARTESIAN_POINT ( 'NONE',  ( 1.882647771056453756, 3.960165260869607629, -32.65113063600000487 ) ) ;
#18223=CARTESIAN_POINT ( 'NONE',  ( 3.950106903291092930, 1.853988655799142959, -1.979170051700004374 ) ) ;
#18226=CARTESIAN_POINT ( 'NONE',  ( 5.093259405240584847, 0.3640143666580218373, -15.58204535869999852 ) ) ;
#18227=CARTESIAN_POINT ( 'NONE',  ( -3.554763430470064822, 2.566410659217317924, -34.46696136359999940 ) ) ;
#18247=CARTESIAN_POINT ( 'NONE',  ( -0.8477857712645231469, -5.155403977784983383, -0.7000226607131746492 ) ) ;
#18268=CARTESIAN_POINT ( 'NONE',  ( -4.274305095845718938, 2.229731738857087642, -2.356264356300000085 ) ) ;
#18269=CARTESIAN_POINT ( 'NONE',  ( -0.4514894588696835021, 4.335480228600247621, -25.38903409330000116 ) ) ;
#18289=CARTESIAN_POINT ( 'NONE',  ( -3.845413171441346201, -3.659953273256227213, -0.8157167102000040249 ) ) ;
#18317=CARTESIAN_POINT ( 'NONE',  ( 2.536150288113637963, -3.576595042060325635, -12.12388893670000201 ) ) ;
#18379=CARTESIAN_POINT ( 'NONE',  ( 3.123710955063047745, -2.074832491810059132, -36.45875473020001323 ) ) ;
#18393=CARTESIAN_POINT ( 'NONE',  ( 4.345117593642236820, 2.039387521354418809, -1.541670051700000377 ) ) ;
#18396=CARTESIAN_POINT ( 'NONE',  ( -4.278952157217899455, -0.8066629416743122949, -16.59949426530001304 ) ) ;
#18397=CARTESIAN_POINT ( 'NONE',  ( 3.956700543085249322, -2.628121156294186633, -34.95875473020000612 ) ) ;
#18413=CARTESIAN_POINT ( 'NONE',  ( 0.6094692351073999204, -5.151249438444421180, -0.7000440620407059056 ) ) ;
#18433=CARTESIAN_POINT ( 'NONE',  ( 4.116710911288352648, -1.508563155650267884, -5.836105321700007842 ) ) ;
#18434=CARTESIAN_POINT ( 'NONE',  ( -6.202057249109299342, 1.908294659314309305, -22.32289663399999924 ) ) ;
#18451=CARTESIAN_POINT ( 'NONE',  ( -1.058439502263211374, 6.005994971325610443, -19.83583244400000112 ) ) ;
#18473=CARTESIAN_POINT ( 'NONE',  ( 3.550610403408205329, -5.007233058897099021, -12.12388893670000201 ) ) ;
#18476=VERTEX_POINT ( 'NONE', #3214 ) ;
#18517=CARTESIAN_POINT ( 'NONE',  ( 4.334836395473461224, -2.879286697580460519, -35.69999999999999574 ) ) ;
#18547=CARTESIAN_POINT ( 'NONE',  ( 1.699015317690025118, 6.330513620609809600, -1.453410702900004292 ) ) ;
#18552=CARTESIAN_POINT ( 'NONE',  ( -2.183849900456023896, 3.899926742306373928, -16.67761783620000315 ) ) ;
#18553=CARTESIAN_POINT ( 'NONE',  ( -4.901082056047598279, -4.330235462250267453, -33.23447003409999212 ) ) ;
#18581=CARTESIAN_POINT ( 'NONE',  ( 3.742179766445304256, 0.3990864396118201651, -35.70000000000000284 ) ) ;
#18590=CARTESIAN_POINT ( 'NONE',  ( -1.641527485091622385, 5.277626912542655369, -5.774955258300002114 ) ) ;
#18591=CARTESIAN_POINT ( 'NONE',  ( 3.710789578725101734, 2.835545959904678170, -23.36727430110000014 ) ) ;
#18607=CARTESIAN_POINT ( 'NONE',  ( 4.904813032679735230, 3.691647504909488564, -32.36032172560000930 ) ) ;
#18627=CARTESIAN_POINT ( 'NONE',  ( 0.7763070146520694159, 4.277613328189615594, -13.52400681850000197 ) ) ;
#18640=ADVANCED_FACE ( 'NONE', ( #7703 ), #12716, .T. ) ;
#18700=CARTESIAN_POINT ( 'NONE',  ( -1.295942751353772238, 4.166547562507297187, -4.774955258300003891 ) ) ;
#18705=CARTESIAN_POINT ( 'NONE',  ( 5.782996427689181651, 1.709881257618839356, -17.54190840230000603 ) ) ;
#18726=CARTESIAN_POINT ( 'NONE',  ( 3.540054785840129892, -1.372664319004998745, -35.69999999999999574 ) ) ;
#18733=CARTESIAN_POINT ( 'NONE',  ( 1.914928416346060702, 3.478121177954408783, -35.69999999999998863 ) ) ;
#18742=CARTESIAN_POINT ( 'NONE',  ( -1.425537026491585868, 4.583202318768851313, -5.712455258300007443 ) ) ;
#18743=CARTESIAN_POINT ( 'NONE',  ( -4.856400125594941386, 3.359828160699422472, -24.46779765530000361 ) ) ;
#18759=CARTESIAN_POINT ( 'NONE',  ( -3.251750336246070461, -5.089746299513510763, -21.70891267860000795 ) ) ;
#18776=CARTESIAN_POINT ( 'NONE',  ( 5.131765537970109037, -1.193580270428616696, -35.69999999999999574 ) ) ;
#18779=CARTESIAN_POINT ( 'NONE',  ( 0.9833222185976336904, 5.418310215658684648, -13.02400681849999842 ) ) ;
#18816=UNCERTAINTY_MEASURE_WITH_UNIT (LENGTH_MEASURE( 1.000000000000000082E-05 ), #26854, 'distance_accuracy_value', 'NONE');
#18844=ORIENTED_EDGE ( 'NONE', *, *, #25496, .F. ) ;
#18860=CARTESIAN_POINT ( 'NONE',  ( -3.052679639724403593, 3.117809041995149411, -4.068732180600004078 ) ) ;
#18865=CARTESIAN_POINT ( 'NONE',  ( 5.320018516182488000, -2.211191048809329374, -17.87122516810000405 ) ) ;
#18896=CARTESIAN_POINT ( 'NONE',  ( 1.388368458387652105, 3.811721462276582706, -35.69999999999999574 ) ) ;
#18901=CARTESIAN_POINT ( 'NONE',  ( 4.781918068392163157, 0.6270375808061986467, -6.564479598400001059 ) ) ;
#18902=CARTESIAN_POINT ( 'NONE',  ( 2.499950477468926291, 3.566222500441432075, -29.21106724380000230 ) ) ;
#18907=CARTESIAN_POINT ( 'NONE',  ( 3.904508939291361003, -1.994718106397497914, -11.91474735220000092 ) ) ;
#18917=CARTESIAN_POINT ( 'NONE',  ( -2.496099253731141943, 5.577352528212363048, -22.73780126169999605 ) ) ;
#18934=CARTESIAN_POINT ( 'NONE',  ( 5.213923276575050281, -0.6319207471432233270, -35.69999999999999574 ) ) ;
#18938=CARTESIAN_POINT ( 'NONE',  ( 4.315341029122434335, -4.279276102762477940, -15.06112212870000455 ) ) ;
#19014=CARTESIAN_POINT ( 'NONE',  ( -2.564224011386423641, 5.541743391105337757, -7.731725184300000997 ) ) ;
#19020=CARTESIAN_POINT ( 'NONE',  ( -4.663991843195165465, -3.413757688390889555, -18.87254627010000263 ) ) ;
#19050=CARTESIAN_POINT ( 'NONE',  ( 0.2160344365416065338, 4.544544668867353643, -35.69999999999999574 ) ) ;
#19059=CARTESIAN_POINT ( 'NONE',  ( -3.993179150428259661, -2.644027878211168581, -7.827429326000001630 ) ) ;
#19060=CARTESIAN_POINT ( 'NONE',  ( 3.499930668453409055, 4.992711500635231836, -28.61106724379999733 ) ) ;
#19065=CARTESIAN_POINT ( 'NONE',  ( -2.507187057889194381, 3.594686560818127763, -1.627651354100000169 ) ) ;
#19076=CARTESIAN_POINT ( 'NONE',  ( -5.902313038799129608, -1.548398769286710053, -25.04656121680000425 ) ) ;
#19099=CARTESIAN_POINT ( 'NONE',  ( 4.813350086082918367, -2.000601425115993148, -16.87122516810000405 ) ) ;
#19124=CARTESIAN_POINT ( 'NONE',  ( 1.984841800599668638, 5.152205253018144582, -27.09462237480000368 ) ) ;
#19173=CARTESIAN_POINT ( 'NONE',  ( -1.295942751353782674, 4.166547562507306957, -4.274955258300005667 ) ) ;
#19177=CARTESIAN_POINT ( 'NONE',  ( 0.7420639427752478978, -6.011517603930927045, -18.37054674910000429 ) ) ;
#19206=CARTESIAN_POINT ( 'NONE',  ( 0.3588211391109571990, 4.320110723951459342, -35.69999999999998863 ) ) ;
#19214=CARTESIAN_POINT ( 'NONE',  ( 3.486358836775546699, -2.566383416802847872, -9.472776792900003073 ) ) ;
#19215=CARTESIAN_POINT ( 'NONE',  ( 0.6138679561251692007, 4.311712124478117580, -29.00600711720001357 ) ) ;
#19221=CARTESIAN_POINT ( 'NONE',  ( 2.521631941452523229, 3.946033397249450125, -5.200967428500000267 ) ) ;
#19249=CARTESIAN_POINT ( 'NONE',  ( 2.917755696240735386, -4.045878105792589885, -0.6999995769812824564 ) ) ;
#19253=CARTESIAN_POINT ( 'NONE',  ( -2.345194346458623347, -4.011532291445385923, -15.18182079290000530 ) ) ;
#19275=STYLED_ITEM ( 'NONE', ( #7953 ), #25297 ) ;
#19280=CARTESIAN_POINT ( 'NONE',  ( -3.878879136156900387, -1.961445906012333928, -28.46472909259999895 ) ) ;
#19330=CARTESIAN_POINT ( 'NONE',  ( -4.484282906631567478, 1.269983465873030015, -7.310827254900003069 ) ) ;
#19336=CARTESIAN_POINT ( 'NONE',  ( 0.5300456733980305479, -4.293941145674102344, -18.87054674910000074 ) ) ;
#19350=CARTESIAN_POINT ( 'NONE',  ( 1.602200344400662058, -4.514849430718075318, -31.19382401680000072 ) ) ;
#19365=DIRECTION ( 'NONE',  ( -0.8329895880221871440, 0.5532886644841251700, 0.000000000000000000 ) ) ;
#19367=CARTESIAN_POINT ( 'NONE',  ( 0.5587536515777949964, 4.694595604172856262, -35.69999999999999574 ) ) ;
#19373=B_SPLINE_CURVE_WITH_KNOTS ( 'NONE', 5,
 ( #11520, #8677, #25536, #3972, #4904, #23959, #19065, #509, #11834, #21434, #2546, #6950, #11980, #28662, #31026, #7108, #19221, #7414, #28803, #19382, #21906, #28505, #26765, #24106, #22058, #352, #9463, #191, #12294, #26613, #21592, #9620, #17013, #12132, #12438, #18907, #19539, #21739, #28971, #14816, #29122, #16693, #26305, #9781, #2847, #16545, #16856, #5054, #7566, #14361, #5201, #2393, #4755, #40, #9935, #17158, #14663, #7266, #26462, #24249, #24414, #26154, #2693, #4586, #14510, #14194, #23797, #2244, #7865, #3607, #27382, #5512, #27526, #10245, #5821, #17468, #29896, #22661, #22202, #17917, #15419, #8021, #19687, #24874, #13203, #22815, #10697, #3303, #20148, #5973, #20292, #658, #29272, #19849, #10093, #8166, #12748, #27075, #15117, #15566, #29430, #24714, #3003, #12595, #3453, #1105, #25021, #29586 ),
 .UNSPECIFIED., .F., .F.,
 ( 6, 3, 3, 3, 3, 3, 3, 3, 3, 3, 3, 3, 3, 3, 3, 3, 3, 3, 3, 3, 3, 3, 3, 3, 3, 3, 3, 3, 3, 3, 3, 3, 3, 3, 3, 6 ),
 ( 8.193316113689999014, 11.38862009670000042, 23.17260734260000277, 34.79167593860000096, 46.25425528950000853, 57.87229377410000097, 69.67120816000000616, 81.20502170430000888, 92.80704244429999505, 104.1208912059999960, 115.9269080290000034, 127.3307717769999812, 139.1306782750000082, 150.7654282180000109, 162.2434640489999822, 173.6637378899999931, 185.2020570420000070, 194.1769840819999899, 203.3038760180000111, 212.5853790139999830, 224.1393301889999918, 235.6932813650000469, 246.8715721779999797, 258.4996770380000157, 270.1277818960000445, 281.7035649139999691, 293.2822232819999613, 304.6732510989999696, 316.1434960830000023, 327.6894369340000139, 339.2353777880000507, 350.7813186390000055, 362.5843219139999860, 374.0573691039999744, 385.8560256170000002, 394.7457478480000077 ),
 .UNSPECIFIED. ) ;
#19374=CARTESIAN_POINT ( 'NONE',  ( 0.2392016894930265591, 6.101552847015987879, -7.937690181100006903 ) ) ;
#19375=CARTESIAN_POINT ( 'NONE',  ( 3.166603938121563377, 4.517215167231739770, -28.21106724380000585 ) ) ;
#19382=CARTESIAN_POINT ( 'NONE',  ( 1.604951280288043014, -4.392199147046020435, -6.260585232200001293 ) ) ;
#19410=CARTESIAN_POINT ( 'NONE',  ( -5.853056545089267537, 1.703994407032248581, -16.30443125759999745 ) ) ;
#19434=CARTESIAN_POINT ( 'NONE',  ( 4.370697773661015972, 1.580342671372847230, -27.01249766020000109 ) ) ;
#19464=STYLED_ITEM ( 'NONE', ( #24934 ), #890 ) ;
#19485=CARTESIAN_POINT ( 'NONE',  ( 6.034652528523337445, 2.501332855249893683, -11.49261350020000449 ) ) ;
#19491=CARTESIAN_POINT ( 'NONE',  ( 6.096654317658788180, 0.1519075334363156893, -21.27661200060000724 ) ) ;
#19506=CARTESIAN_POINT ( 'NONE',  ( 0.8594151385421661127, 6.036396974313712249, -29.60600711720000433 ) ) ;
#19521=CARTESIAN_POINT ( 'NONE',  ( 1.171347117349504252, 4.722363560431488416, -35.69999999999999574 ) ) ;
#19524=CARTESIAN_POINT ( 'NONE',  ( -3.779681388771212180, -0.7623632300730877054, -0.6999999999999992895 ) ) ;
#19528=CARTESIAN_POINT ( 'NONE',  ( 3.619519562537643065, 2.908736503316577959, -8.354586408000006514 ) ) ;
#19529=CARTESIAN_POINT ( 'NONE',  ( -1.266353310550808464, -4.943458602710906646, -26.61132611460000064 ) ) ;
#19539=CARTESIAN_POINT ( 'NONE',  ( 2.536150288113637963, -3.576595042060325635, -12.12388893670000201 ) ) ;
#19567=CARTESIAN_POINT ( 'NONE',  ( -2.579713781069702616, -4.412685520613435664, -14.74432079290000175 ) ) ;
#19592=CARTESIAN_POINT ( 'NONE',  ( -5.902313038799129608, -1.548398769286710053, -25.64656121680000567 ) ) ;
#19610=CARTESIAN_POINT ( 'NONE',  ( 3.339648724517960687, -2.614705901102248209, -0.6999999999999992895 ) ) ;
#19636=CARTESIAN_POINT ( 'NONE',  ( 3.486358836775546699, -2.566383416802847872, -8.472776792899997744 ) ) ;
#19644=CARTESIAN_POINT ( 'NONE',  ( 5.503465972402116435, -2.627571514392686769, -21.48180150030000490 ) ) ;
#19653=CARTESIAN_POINT ( 'NONE',  ( 3.653275382406361071, -2.426579979385206531, -0.6999999999999992895 ) ) ;
#19658=CARTESIAN_POINT ( 'NONE',  ( 2.039164074698236906, -5.746172002732055084, -30.85632401679999504 ) ) ;
#19678=CARTESIAN_POINT ( 'NONE',  ( 3.112737406813101515, -4.802415649948616583, -0.1659393883000001568 ) ) ;
#19680=CARTESIAN_POINT ( 'NONE',  ( 0.3986823046148949556, -5.109930552333694642, -10.33088421180000083 ) ) ;
#19681=CARTESIAN_POINT ( 'NONE',  ( 2.039164074698236906, -5.746172002732055084, -30.25632401680000783 ) ) ;
#19687=CARTESIAN_POINT ( 'NONE',  ( -1.151230282303593366, -4.494053275198268693, -27.54882611460000774 ) ) ;
#19723=CARTESIAN_POINT ( 'NONE',  ( 1.403799475828179766, 5.569137675590418723, -17.05080441500000177 ) ) ;
#19730=DIRECTION ( 'NONE',  ( 0.000000000000000000, 0.000000000000000000, 1.000000000000000000 ) ) ;
#19747=CARTESIAN_POINT ( 'NONE',  ( -4.555585884337687297, -4.059738318096004939, -25.44101932449999026 ) ) ;
#19766=CARTESIAN_POINT ( 'NONE',  ( 3.164224794202841640, -2.738734268234706448, -0.6999999999999992895 ) ) ;
#19795=CARTESIAN_POINT ( 'NONE',  ( -4.184186767956295405, -1.312611723764782523, -10.02323088899999881 ) ) ;
#19800=CARTESIAN_POINT ( 'NONE',  ( -5.611385130160316592, 1.726552310816597435, -23.32289663400000990 ) ) ;
#19817=CARTESIAN_POINT ( 'NONE',  ( -5.305719984766040120, 1.510612064730647131, -32.30158078970000446 ) ) ;
#19835=CARTESIAN_POINT ( 'NONE',  ( -4.364338366759058729, 2.011379601984358612, -0.6999999999999991784 ) ) ;
#19840=CARTESIAN_POINT ( 'NONE',  ( 3.981471518793421538, 3.199610153647690414, -9.292086407999997633 ) ) ;
#19841=CARTESIAN_POINT ( 'NONE',  ( 2.022420680230010870, -3.847796821814265300, -32.70721934060000535 ) ) ;
#19849=CARTESIAN_POINT ( 'NONE',  ( -4.188726303739433554, 1.192588472141202560, -31.30158078970000801 ) ) ;
#19866=ORIENTED_EDGE ( 'NONE', *, *, #27460, .F. ) ;
#19878=CARTESIAN_POINT ( 'NONE',  ( -3.665401116828205463, 4.874126016103034864, -19.63064294430000345 ) ) ;
#19920=CARTESIAN_POINT ( 'NONE',  ( 1.035314575941623572, -3.725342087822672621, -0.6999999999999994005 ) ) ;
#19948=CARTESIAN_POINT ( 'NONE',  ( -2.554946692801202346, -3.999086378171832212, -22.64641267860000085 ) ) ;
#19962=CARTESIAN_POINT ( 'NONE',  ( 1.456545767631101107, -4.104408573385627257, -30.25632401680000783 ) ) ;
#19977=CARTESIAN_POINT ( 'NONE',  ( -3.925832445961813910, 0.9642144021018008715, -0.6999999999999992895 ) ) ;
#19982=CARTESIAN_POINT ( 'NONE',  ( 2.618538529469180531, 3.470429992801026042, -14.22796858840000311 ) ) ;
#19983=CARTESIAN_POINT ( 'NONE',  ( 4.420334067734101424, -4.199682076162645217, -29.45126389020000346 ) ) ;
#20005=EDGE_LOOP ( 'NONE', ( #29566, #21265, #19866, #25388, #21105, #1713 ) ) ;
#20021=CARTESIAN_POINT ( 'NONE',  ( -3.175770273322759518, 4.553269643686719270, -2.627651354100001946 ) ) ;
#20022=CARTESIAN_POINT ( 'NONE',  ( -3.117834729128555971, -4.866792379758847709, -18.70544088820000184 ) ) ;
#20038=CARTESIAN_POINT ( 'NONE',  ( -3.010188847176034521, -5.300177380992629139, -6.685065142700001850 ) ) ;
#20059=SURFACE_STYLE_FILL_AREA ( #17222 ) ;
#20109=CARTESIAN_POINT ( 'NONE',  ( -3.679974273075534708, -2.251605409995533602, -22.40799200640001132 ) ) ;
#20123=CARTESIAN_POINT ( 'NONE',  ( 4.904813032679735230, 3.691647504909488564, -32.36032172560000930 ) ) ;
#20137=CARTESIAN_POINT ( 'NONE',  ( -3.745245862513339574, 2.150978246590952825, -0.6999999999999991784 ) ) ;
#20141=CARTESIAN_POINT ( 'NONE',  ( 1.348918213770415653, 4.124136235849971577, -11.07047964830000453 ) ) ;
#20142=CARTESIAN_POINT ( 'NONE',  ( 3.853781668572211938, 2.900580182403568408, -31.42282172560000575 ) ) ;
#20148=CARTESIAN_POINT ( 'NONE',  ( 4.634019325638262465, 0.4639887426745106791, -29.63116556699998938 ) ) ;
#20175=CARTESIAN_POINT ( 'NONE',  ( -4.325159770583743679, -1.744232581393518666, -1.497197434500001867 ) ) ;
#20176=CARTESIAN_POINT ( 'NONE',  ( 1.771049722044198971, -6.234229536879996481, -20.69535708930001050 ) ) ;
#20189=CARTESIAN_POINT ( 'NONE',  ( -4.663991843195165465, -3.413757688390889555, -18.87254627010000263 ) ) ;
#20219=CARTESIAN_POINT ( 'NONE',  ( 3.600464914056809018, -2.449529153870059872, -0.6999999999999992895 ) ) ;
#20247=CARTESIAN_POINT ( 'NONE',  ( 4.266075142677475007, -0.9221078188639888484, -23.79036215650000230 ) ) ;
#20265=CARTESIAN_POINT ( 'NONE',  ( -4.901082056047598279, -4.330235462250267453, -33.83447003409999354 ) ) ;
#20281=CARTESIAN_POINT ( 'NONE',  ( -3.789431608055533474, 1.866661010915773744, -0.6999999999999994005 ) ) ;
#20285=CARTESIAN_POINT ( 'NONE',  ( -1.184025259985578948, -4.532227402022654061, -13.05022317840000312 ) ) ;
#20286=CARTESIAN_POINT ( 'NONE',  ( 2.561732861596754507, -4.873875974289409108, -32.20721934060000535 ) ) ;
#20292=CARTESIAN_POINT ( 'NONE',  ( 1.456545767631101107, -4.104408573385627257, -30.25632401680000783 ) ) ;
#20327=CARTESIAN_POINT ( 'NONE',  ( -5.440024667461782037, 2.837840394948672351, -1.418764356299999418 ) ) ;
#20328=CARTESIAN_POINT ( 'NONE',  ( 6.096654317658788180, 0.1519075334363156893, -20.67661200060000226 ) ) ;
#20344=CARTESIAN_POINT ( 'NONE',  ( 1.086829820489895848, 5.988658659452708477, -14.02400681850000197 ) ) ;
#20368=CARTESIAN_POINT ( 'NONE',  ( -4.345037505360560992, 2.733239894040710105, -9.507975902800009038 ) ) ;
#20380=CARTESIAN_POINT ( 'NONE',  ( 5.245096043587340162, -0.2338077457563897399, -35.69999999999999574 ) ) ;
#20423=CARTESIAN_POINT ( 'NONE',  ( -4.434312336397093546, -3.917832084918029256, -34.83447003410000065 ) ) ;
#20438=CARTESIAN_POINT ( 'NONE',  ( -5.068867860199277153, -0.8055594120499698363, -0.6999999999999992895 ) ) ;
#20439=CARTESIAN_POINT ( 'NONE',  ( 4.080592064681261455, -5.083854565965863159, -2.505321867100007704 ) ) ;
#20443=CARTESIAN_POINT ( 'NONE',  ( -4.799781135534763266, 0.1424267153701331001, -14.12054957890000040 ) ) ;
#20444=CARTESIAN_POINT ( 'NONE',  ( 0.1051796283266584475, -6.084780997910130829, -33.41110030499999795 ) ) ;
#20483=CARTESIAN_POINT ( 'NONE',  ( -4.921927080085812811, 2.567569881136803733, -2.418764356300004970 ) ) ;
#20484=CARTESIAN_POINT ( 'NONE',  ( -4.430040892179064826, 1.363067613765865937, -21.82289663400000279 ) ) ;
#20500=CARTESIAN_POINT ( 'NONE',  ( 5.320018516182488000, -2.211191048809329374, -17.87122516810000405 ) ) ;
#20522=CARTESIAN_POINT ( 'NONE',  ( 1.708629737455300335, 5.223905898740939691, -10.07047964830000097 ) ) ;
#20582=CARTESIAN_POINT ( 'NONE',  ( 4.417684705200791484, 4.247747620870205409, -35.92341724620000321 ) ) ;
#20597=CARTESIAN_POINT ( 'NONE',  ( -1.102325287918849650, -5.983340188646091740, -2.925234013000002520 ) ) ;
#20601=CARTESIAN_POINT ( 'NONE',  ( 3.904508939291349900, -1.994718106397494362, -12.41474735220000092 ) ) ;
#20602=CARTESIAN_POINT ( 'NONE',  ( 5.877945039781666381, 1.734296231098907182, -35.53159726780000227 ) ) ;
#20634=CARTESIAN_POINT ( 'NONE',  ( 2.885864564934697896, 2.548163973319825359, -35.70000000000000284 ) ) ;
#20641=CARTESIAN_POINT ( 'NONE',  ( 0.6465148687764388225, -4.727082501367554812, -1.310624048000003095 ) ) ;
#20642=CARTESIAN_POINT ( 'NONE',  ( -5.902313038799129608, -1.548398769286710053, -24.44656121679999927 ) ) ;
#20662=CARTESIAN_POINT ( 'NONE',  ( -4.338779899226326009, -4.343559731693466652, -9.813991631000003935 ) ) ;
#20684=CARTESIAN_POINT ( 'NONE',  ( -6.108812354267502798, 0.1812703649498176306, -12.58304957890000253 ) ) ;
#20741=CARTESIAN_POINT ( 'NONE',  ( 0.1051796283266584475, -6.084780997910130829, -34.01110030499999937 ) ) ;
#20753=CARTESIAN_POINT ( 'NONE',  ( -4.439228537916153350, -2.748747741535113587, -0.6999999999999992895 ) ) ;
#20754=CARTESIAN_POINT ( 'NONE',  ( -2.624260084387262104, -3.463915187244965388, -3.228945369299999868 ) ) ;
#20759=CARTESIAN_POINT ( 'NONE',  ( 6.482330152203070739, 0.4632910120546396282, -15.24454535870000527 ) ) ;
#20760=CARTESIAN_POINT ( 'NONE',  ( 4.618385388201741826, 1.362661324479865099, -34.59409726779999517 ) ) ;
#20778=CARTESIAN_POINT ( 'NONE',  ( -0.6848972644784130370, -5.175796693238598145, -0.7000250125985852945 ) ) ;
#20800=CARTESIAN_POINT ( 'NONE',  ( 5.214500487626152037, -1.910846663805727541, -6.836105321700002513 ) ) ;
#20801=CARTESIAN_POINT ( 'NONE',  ( 5.972505199797514486, -1.290950946386169917, -23.19036215650000088 ) ) ;
#20818=CARTESIAN_POINT ( 'NONE',  ( 6.379535387291454640, -1.442012952481606991, -32.78377053309999667 ) ) ;
#20845=CARTESIAN_POINT ( 'NONE',  ( -1.184025259985572953, -4.532227402022651397, -12.55022317840000312 ) ) ;
#20918=CARTESIAN_POINT ( 'NONE',  ( -3.950471790850672793, -3.522405822398885888, -0.6999999999999992895 ) ) ;
#20919=CARTESIAN_POINT ( 'NONE',  ( 5.530149664617865390, 2.595584118083901881, -1.879170051700004951 ) ) ;
#20923=CARTESIAN_POINT ( 'NONE',  ( -5.853056545089267537, 1.703994407032248581, -16.30443125759999745 ) ) ;
#20924=CARTESIAN_POINT ( 'NONE',  ( -0.4593365651765490831, 6.553622599173768215, -34.89518930509999706 ) ) ;
#20937=CARTESIAN_POINT ( 'NONE',  ( -0.6108973618901316627, -5.182830691052390470, -0.7000282472846792725 ) ) ;
#20956=CARTESIAN_POINT ( 'NONE',  ( -1.814319851916122772, 5.833166587536846137, -5.374955258299999983 ) ) ;
#20957=CARTESIAN_POINT ( 'NONE',  ( 0.09521150875770739708, -4.665041947735808492, -24.41888333260000365 ) ) ;
#20969=MECHANICAL_DESIGN_GEOMETRIC_PRESENTATION_REPRESENTATION('',(#19464),#5878);
#20974=CARTESIAN_POINT ( 'NONE',  ( 2.193772516446764076, 5.694542648089183423, -26.09462237480000724 ) ) ;
#20979=EDGE_LOOP ( 'NONE', ( #22790, #21337, #24823, #28210 ) ) ;
#20998=CARTESIAN_POINT ( 'NONE',  ( -1.657635364023947400, -6.345118362804027079, -12.55022317840000312 ) ) ;
#21077=CARTESIAN_POINT ( 'NONE',  ( -4.325159770583737462, -1.744232581393518444, -0.9971974345000036433 ) ) ;
#21081=CARTESIAN_POINT ( 'NONE',  ( 3.256742448429973624, 4.730705660258329281, -17.81259163650000232 ) ) ;
#21105=ORIENTED_EDGE ( 'NONE', *, *, #25496, .T. ) ;
#21109=CARTESIAN_POINT ( 'NONE',  ( 2.105781777274182698, 3.334946656835463319, -35.69999999999999574 ) ) ;
#21116=CARTESIAN_POINT ( 'NONE',  ( -0.7873752056533391830, -4.273814420472604070, -4.025234013000003053 ) ) ;
#21117=CARTESIAN_POINT ( 'NONE',  ( 4.692682656939434871, -1.014318600726540787, -22.85286215650000585 ) ) ;
#21133=CARTESIAN_POINT ( 'NONE',  ( 3.241815827827634777, 4.728971459636320596, -35.21970670789999502 ) ) ;
#21148=CARTESIAN_POINT ( 'NONE',  ( 1.896306263639558010, -4.736092137553404413, -0.7000633247167794559 ) ) ;
#21152=CARTESIAN_POINT ( 'NONE',  ( -5.517889265940039145, -2.627421812126006451, -12.37655742009999926 ) ) ;
#21199=DIRECTION ( 'NONE',  ( -0.8329895880221872551, 0.5532886644841250590, 0.000000000000000000 ) ) ;
#21223=CARTESIAN_POINT ( 'NONE',  ( -3.630162863991666988, -2.403661707492382060, -6.389929326000004295 ) ) ;
#21228=CARTESIAN_POINT ( 'NONE',  ( 2.558869066659682723, 3.716983018758990287, -18.15009163650000090 ) ) ;
#21265=ORIENTED_EDGE ( 'NONE', *, *, #17254, .F. ) ;
#21266=CARTESIAN_POINT ( 'NONE',  ( 1.604951280288043014, -4.392199147046020435, -6.260585232200001293 ) ) ;
#21267=CARTESIAN_POINT ( 'NONE',  ( -1.782928038406566884, 3.983823234458335527, -22.23780126169999960 ) ) ;
#21307=CARTESIAN_POINT ( 'NONE',  ( 1.757687669117797835, -5.210066540036287996, -14.26414732020001175 ) ) ;
#21337=ORIENTED_EDGE ( 'NONE', *, *, #7989, .T. ) ;
#21353=ADVANCED_FACE ( 'NONE', ( #16317 ), #27807, .F. ) ;
#21386=CARTESIAN_POINT ( 'NONE',  ( -2.150134890876696847, -3.785840986416655340, -6.685065142700001850 ) ) ;
#21392=CARTESIAN_POINT ( 'NONE',  ( 4.190083271568243894, -3.954132654168471817, -18.63565260999999751 ) ) ;
#21423=CARTESIAN_POINT ( 'NONE',  ( 1.552911329599348633, 4.674210618965234154, -35.70000000000000284 ) ) ;
#21428=CARTESIAN_POINT ( 'NONE',  ( -2.365148379994555849, -4.164425085035065699, -7.622565142700000074 ) ) ;
#21429=CARTESIAN_POINT ( 'NONE',  ( 2.499950477468915189, 3.566222500441431187, -28.71106724380000230 ) ) ;
#21434=CARTESIAN_POINT ( 'NONE',  ( 4.360957369889326252, -0.1505632777267507105, -2.685409721200002320 ) ) ;
#21440=CARTESIAN_POINT ( 'NONE',  ( -5.151963982244392781, -3.152247574024123811, -21.90799200640000777 ) ) ;
#21460=CARTESIAN_POINT ( 'NONE',  ( 5.245096043587340162, -0.2338077457563897399, -35.69999999999999574 ) ) ;
#21464=CARTESIAN_POINT ( 'NONE',  ( 3.256742448429973624, 4.730705660258329281, -17.21259163649999735 ) ) ;
#21520=CARTESIAN_POINT ( 'NONE',  ( 4.373195337096333013, -2.904765488536246387, -36.55875473019999333 ) ) ;
#21539=CARTESIAN_POINT ( 'NONE',  ( 0.2392016894930265591, 6.101552847015987879, -7.337690181100003706 ) ) ;
#21544=CARTESIAN_POINT ( 'NONE',  ( 2.992916622598570608, -2.824380467281231599, -18.53565260999999609 ) ) ;
#21578=CARTESIAN_POINT ( 'NONE',  ( 0.2009654409541410391, 4.469944785342635285, -35.69999999999999574 ) ) ;
#21581=CARTESIAN_POINT ( 'NONE',  ( -3.806419540421088321, -0.6621889094791760799, -0.6999999999999992895 ) ) ;
#21585=CARTESIAN_POINT ( 'NONE',  ( -5.857861475075242019, -1.837656413297739766, -10.62323088900000378 ) ) ;
#21586=CARTESIAN_POINT ( 'NONE',  ( -1.151230282303595587, -4.494053275198272246, -27.04882611459999353 ) ) ;
#21592=CARTESIAN_POINT ( 'NONE',  ( -4.184186767956295405, -1.312611723764782523, -10.02323088899999881 ) ) ;
#21617=CARTESIAN_POINT ( 'NONE',  ( 2.940048186824491872, -4.025564021813598181, -0.6999991271805777737 ) ) ;
#21620=CARTESIAN_POINT ( 'NONE',  ( -2.227024806490494946, -3.476280271252722542, -18.20544088820000184 ) ) ;
#21650=CARTESIAN_POINT ( 'NONE',  ( -5.430430790592723156, -2.746024268427175841, -28.56472909259999327 ) ) ;
#21685=VERTEX_POINT ( 'NONE', #29012 ) ;
#21694=CARTESIAN_POINT ( 'NONE',  ( -2.365148379994555849, -4.164425085035065699, -5.747565142700007179 ) ) ;
#21698=CARTESIAN_POINT ( 'NONE',  ( -4.893571841042398063, 0.6806285466628937408, -20.18909460729999950 ) ) ;
#21711=CARTESIAN_POINT ( 'NONE',  ( -4.607598934103576127, 1.311847319348407481, -32.23908078970000446 ) ) ;
#21725=CARTESIAN_POINT ( 'NONE',  ( 1.013280384041870263, 4.005003068705073943, -35.69999999999998153 ) ) ;
#21727=CARTESIAN_POINT ( 'NONE',  ( -3.937802700299847469, 0.01361741897907296078, -0.6999999999999991784 ) ) ;
#21731=CARTESIAN_POINT ( 'NONE',  ( -2.564224011386423641, 5.541743391105337757, -7.731725184300000997 ) ) ;
#21732=CARTESIAN_POINT ( 'NONE',  ( 2.695668638436317543, -3.937035225248731951, -26.19542313650000054 ) ) ;
#21739=CARTESIAN_POINT ( 'NONE',  ( -1.184025259985572953, -4.532227402022651397, -12.55022317840000312 ) ) ;
#21768=CARTESIAN_POINT ( 'NONE',  ( 3.843992482562140989, -2.627063339010873300, -0.6999999999867967393 ) ) ;
#21772=CARTESIAN_POINT ( 'NONE',  ( -4.278952157217901231, -0.8066629416743145153, -16.09949426530000238 ) ) ;
#21798=CARTESIAN_POINT ( 'NONE',  ( -4.215937884789282108, -1.105999120962573246, -25.54656121680000425 ) ) ;
#21854=CARTESIAN_POINT ( 'NONE',  ( 5.459923716313909381, 2.263110678531865094, -10.49261350019999561 ) ) ;
#21859=CARTESIAN_POINT ( 'NONE',  ( 0.6713911862884133219, -5.438992117826878747, -19.37054674910000074 ) ) ;
#21876=CARTESIAN_POINT ( 'NONE',  ( 3.157381476932436648, -2.999772911539579034, -30.55126389019999777 ) ) ;
#21892=CARTESIAN_POINT ( 'NONE',  ( 0.8241976871332568066, 4.093728295075581336, -35.70000000000000284 ) ) ;
#21898=CARTESIAN_POINT ( 'NONE',  ( 4.880902371519058036, -3.592936783560450653, -8.972776792900004850 ) ) ;
#21899=CARTESIAN_POINT ( 'NONE',  ( 0.7775660777938816492, 5.461502024334397909, -28.00600711720000291 ) ) ;
#21906=CARTESIAN_POINT ( 'NONE',  ( -2.150134890876696847, -3.785840986416655340, -6.685065142700001850 ) ) ;
#21933=CARTESIAN_POINT ( 'NONE',  ( 4.180014548479816128, -1.737364395512316362, -16.93372516810000405 ) ) ;
#21957=CARTESIAN_POINT ( 'NONE',  ( 0.1047326596782457986, -5.131546142535936994, -25.35638333260000010 ) ) ;
#22004=CARTESIAN_POINT ( 'NONE',  ( 1.888485499342153151, 5.773790730162923879, -11.07047964830000453 ) ) ;
#22010=CARTESIAN_POINT ( 'NONE',  ( 5.516020573121914516, 0.1374401492888292498, -21.67661200059999871 ) ) ;
#22029=CARTESIAN_POINT ( 'NONE',  ( 3.499930668453409055, 4.992711500635231836, -29.21106724380000230 ) ) ;
#22043=CARTESIAN_POINT ( 'NONE',  ( 0.7743111960048394415, 4.722446211719187659, -35.69999999999998863 ) ) ;
#22050=CARTESIAN_POINT ( 'NONE',  ( 5.399570250832249840, -0.9558082389699539272, -9.771482634699999892 ) ) ;
#22051=CARTESIAN_POINT ( 'NONE',  ( 0.8594151385421661127, 6.036396974313712249, -28.40600711719999794 ) ) ;
#22058=CARTESIAN_POINT ( 'NONE',  ( 0.1708583496781435063, 4.358252033550405358, -7.937690181100000686 ) ) ;
#22085=CARTESIAN_POINT ( 'NONE',  ( -2.449727287106972184, -3.823908298404834483, -17.76794088820000894 ) ) ;
#22108=CARTESIAN_POINT ( 'NONE',  ( 4.170003719837387379, -2.319039617661839081, -27.86787294500000556 ) ) ;
#22125=CARTESIAN_POINT ( 'NONE',  ( 3.405583316338488320, -2.569273692377948226, -0.6999999999999992895 ) ) ;
#22152=CARTESIAN_POINT ( 'NONE',  ( 4.262818619062177738, -0.7545854518158021662, -8.771482634699998115 ) ) ;
#22159=CARTESIAN_POINT ( 'NONE',  ( -6.202057249109299342, 1.908294659314309305, -22.92289663400000421 ) ) ;
#22172=CARTESIAN_POINT ( 'NONE',  ( 0.8594151385421661127, 6.036396974313712249, -29.00600711719999936 ) ) ;
#22190=CARTESIAN_POINT ( 'NONE',  ( -5.064516463719014538, -0.8477338316829075016, -0.6999999999999992895 ) ) ;
#22191=CARTESIAN_POINT ( 'NONE',  ( 0.8228371056950706253, -6.016286819831330845, 0.2268759520000010466 ) ) ;
#22194=CARTESIAN_POINT ( 'NONE',  ( -2.320012200738846619, 5.013958306206127702, -8.731725184300000109 ) ) ;
#22195=CARTESIAN_POINT ( 'NONE',  ( 2.635706879431563898, 5.544231365240147369, -32.15113063600000487 ) ) ;
#22202=CARTESIAN_POINT ( 'NONE',  ( 1.566980368899947962, 4.067530462867743779, -26.09462237480000724 ) ) ;
#22234=CARTESIAN_POINT ( 'NONE',  ( 3.931047123110464891, -1.876836795983964912, -20.38180150030001059 ) ) ;
#22259=CARTESIAN_POINT ( 'NONE',  ( -0.4966384047618531139, 4.769028251466922441, -26.82653409330000116 ) ) ;
#22277=CARTESIAN_POINT ( 'NONE',  ( 2.553054491426671291, -3.139702421570553792, -0.6999999999999992895 ) ) ;
#22312=CARTESIAN_POINT ( 'NONE',  ( -1.782928038406565774, 3.983823234458339080, -22.73780126169999605 ) ) ;
#22329=CARTESIAN_POINT ( 'NONE',  ( -2.705882613314523955, 5.963358562559473164, -32.32635571290000343 ) ) ;
#22343=CARTESIAN_POINT ( 'NONE',  ( 2.919513974631230191, 4.160045535825797280, -35.69999999999999574 ) ) ;
#22346=CARTESIAN_POINT ( 'NONE',  ( -4.891960740915500594, 0.9743236597107772790, -0.6999999999999992895 ) ) ;
#22354=CARTESIAN_POINT ( 'NONE',  ( -3.222838750790782303, 3.984490938364168233, -14.54102819870000474 ) ) ;
#22355=CARTESIAN_POINT ( 'NONE',  ( 2.384687176697237732, 5.016209330415857259, -31.15113063599999776 ) ) ;
#22393=CARTESIAN_POINT ( 'NONE',  ( 3.956700543085260424, -2.628121156294163541, -0.9587547302000037908 ) ) ;
#22394=CARTESIAN_POINT ( 'NONE',  ( 1.265035515811502309, -4.453021097817297047, -21.29535708919999593 ) ) ;
#22438=CARTESIAN_POINT ( 'NONE',  ( 3.521492630942301361, -2.494370597472697071, -0.6999999999999992895 ) ) ;
#22469=CARTESIAN_POINT ( 'NONE',  ( -2.942059828035410440, -4.605008556695580957, -22.70891267860000085 ) ) ;
#22483=CARTESIAN_POINT ( 'NONE',  ( -1.932773295258167545, 4.259541830411040841, -32.22635571290000911 ) ) ;
#22502=CARTESIAN_POINT ( 'NONE',  ( -3.746730446667854153, 2.137546260429493472, -0.6999999999999992895 ) ) ;
#22509=CARTESIAN_POINT ( 'NONE',  ( 3.904508939291361003, -1.994718106397497914, -11.91474735220000092 ) ) ;
#22510=CARTESIAN_POINT ( 'NONE',  ( 1.882647771056455976, 3.960165260869605408, -32.15113063600000487 ) ) ;
#22547=CARTESIAN_POINT ( 'NONE',  ( -2.757905763689965095, 3.954155216896602987, -2.565151354099997505 ) ) ;
#22548=CARTESIAN_POINT ( 'NONE',  ( 5.503465972402116435, -2.627571514392686769, -20.88180150029999993 ) ) ;
#22563=CARTESIAN_POINT ( 'NONE',  ( -5.517889265940039145, -2.627421812126006451, -12.97655742010000246 ) ) ;
#22595=CARTESIAN_POINT ( 'NONE',  ( 3.367430855165096659, -2.595439161230981728, -0.6999999999999992895 ) ) ;
#22609=EDGE_LOOP ( 'NONE', ( #22713, #10197, #1589, #30779 ) ) ;
#22617=UNCERTAINTY_MEASURE_WITH_UNIT (LENGTH_MEASURE( 1.000000000000000082E-05 ), #10311, 'distance_accuracy_value', 'NONE');
#22625=CARTESIAN_POINT ( 'NONE',  ( 4.266075142677459908, -0.9221078188639819651, -24.29036215650000585 ) ) ;
#22636=CARTESIAN_POINT ( 'NONE',  ( 2.635706879431563898, 5.544231365240147369, -32.15113063600000487 ) ) ;
#22651=CARTESIAN_POINT ( 'NONE',  ( -4.074815451744496109, 2.319135910757860852, -0.6999999999999992895 ) ) ;
#22652=CARTESIAN_POINT ( 'NONE',  ( 0.8228371056950706253, -6.016286819831330845, -0.3731240480000022619 ) ) ;
#22655=CARTESIAN_POINT ( 'NONE',  ( 1.483810035143914297, 4.536549859444123811, -12.00797964829999742 ) ) ;
#22656=CARTESIAN_POINT ( 'NONE',  ( 4.556810990865948874, -1.030009251744163468, -32.28377053310000377 ) ) ;
#22661=CARTESIAN_POINT ( 'NONE',  ( -0.4514894588696777289, 4.335480228600245844, -25.88903409329999761 ) ) ;
#22692=CARTESIAN_POINT ( 'NONE',  ( 5.530149664617865390, 2.595584118083901881, -2.479170051700001043 ) ) ;
#22693=CARTESIAN_POINT ( 'NONE',  ( -3.331422745097509797, -2.438398348906448021, -18.37254627010000974 ) ) ;
#22707=CARTESIAN_POINT ( 'NONE',  ( -5.440024667461782037, 2.837840394948672351, -1.418764356299999418 ) ) ;
#22713=ORIENTED_EDGE ( 'NONE', *, *, #10777, .T. ) ;
#22728=CARTESIAN_POINT ( 'NONE',  ( -0.6370991518874399295, 4.292107257743936977, -10.36772091660000861 ) ) ;
#22750=( NAMED_UNIT ( * ) PLANE_ANGLE_UNIT ( ) SI_UNIT ( $, .RADIAN. ) );
#22771=CARTESIAN_POINT ( 'NONE',  ( 0.3233900739386466605, 6.101867874933233793, -22.94418644579999977 ) ) ;
#22787=CARTESIAN_POINT ( 'NONE',  ( -3.500772897184936561, -3.093025330206538470, -33.83447003410000775 ) ) ;
#22790=ORIENTED_EDGE ( 'NONE', *, *, #17254, .T. ) ;
#22795=SHAPE_DEFINITION_REPRESENTATION ( #5637, #16405 ) ;
#22801=CARTESIAN_POINT ( 'NONE',  ( 5.181945990355393050, 1.017753073738105751, -35.69999999999998863 ) ) ;
#22804=CARTESIAN_POINT ( 'NONE',  ( -3.745223230361195643, 2.151215814118476732, -0.6999999999999992895 ) ) ;
#22805=CARTESIAN_POINT ( 'NONE',  ( 3.206179479465854243, -3.994457159022797299, -2.167821867100002908 ) ) ;
#22808=CARTESIAN_POINT ( 'NONE',  ( -3.941349475653407985, -1.876729865818548282, -13.47655742010000601 ) ) ;
#22809=CARTESIAN_POINT ( 'NONE',  ( -4.502700345321055231, 3.250786835042839051, -33.46696136359999230 ) ) ;
#22815=CARTESIAN_POINT ( 'NONE',  ( -3.052438874386664835, 3.509528713898347974, -28.58728588869999143 ) ) ;
#22850=CARTESIAN_POINT ( 'NONE',  ( -6.055223678858003389, -2.441925613954294860, -0.9971974345000036433 ) ) ;
#22851=CARTESIAN_POINT ( 'NONE',  ( -4.661300745830698311, -2.852033519371924619, -20.90799200640000777 ) ) ;
#22871=CARTESIAN_POINT ( 'NONE',  ( -5.853056545089267537, 1.703994407032248581, -16.30443125759999745 ) ) ;
#22875=ORIENTED_EDGE ( 'NONE', *, *, #27460, .T. ) ;
#22892=CARTESIAN_POINT ( 'NONE',  ( 1.888485499342153151, 5.773790730162923879, -10.47047964830000133 ) ) ;
#22950=CARTESIAN_POINT ( 'NONE',  ( -4.502700345321055231, 3.250786835042839051, -35.46696136359999940 ) ) ;
#22966=CARTESIAN_POINT ( 'NONE',  ( -0.8661127261961210078, -4.701195862525644031, -2.587734013000004829 ) ) ;
#22970=CARTESIAN_POINT ( 'NONE',  ( 0.7763070146520694159, 4.277613328189615594, -14.52400681850000730 ) ) ;
#22989=CARTESIAN_POINT ( 'NONE',  ( 1.199321674214643529, -5.002983764577906278, -0.6999981557156819134 ) ) ;
#22996=CARTESIAN_POINT ( 'NONE',  ( 3.659488124655024599, -0.9781774386366028917, -35.69999999999999574 ) ) ;
#23000=CARTESIAN_POINT ( 'NONE',  ( 1.271866015585619403, 3.874426768252950737, -35.70000000000000284 ) ) ;
#23009=CARTESIAN_POINT ( 'NONE',  ( -2.507187057889202819, 3.594686560818132204, -2.127651354099999725 ) ) ;
#23010=CARTESIAN_POINT ( 'NONE',  ( -4.121720561938956529, -3.673096573571036139, -23.84101932449999950 ) ) ;
#23029=CARTESIAN_POINT ( 'NONE',  ( 5.466312515054250198, -2.792605348973308477, -11.91474735220000092 ) ) ;
#23053=CARTESIAN_POINT ( 'NONE',  ( 0.8539377161337347033, 4.705374660993639324, -13.08650681850000730 ) ) ;
#23115=CLOSED_SHELL ( 'NONE', ( #29375, #21353, #25500, #18640, #8665, #17419 ) ) ;
#23116=CARTESIAN_POINT ( 'NONE',  ( 2.070912548172440637, 4.356181786950492629, -33.08863063599999776 ) ) ;
#23131=CARTESIAN_POINT ( 'NONE',  ( -1.102325287918849650, -5.983340188646091740, -3.525234013000005717 ) ) ;
#23134=CARTESIAN_POINT ( 'NONE',  ( -2.183849900456024784, 3.899926742306370819, -17.17761783620000315 ) ) ;
#23135=CARTESIAN_POINT ( 'NONE',  ( -0.4593365651765490831, 6.553622599173768215, -34.29518930510000274 ) ) ;
#23168=CARTESIAN_POINT ( 'NONE',  ( -1.814319851916122772, 5.833166587536846137, -4.774955258300003891 ) ) ;
#23169=CARTESIAN_POINT ( 'NONE',  ( 0.1332961122732720383, -6.531058726825651028, -23.81888333260000223 ) ) ;
#23184=CARTESIAN_POINT ( 'NONE',  ( 1.771049722044198971, -6.234229536879996481, -21.29535708919999593 ) ) ;
#23207=CARTESIAN_POINT ( 'NONE',  ( 5.864965375735811115, 0.4191680585659274261, -13.64454535870001095 ) ) ;
#23254=CARTESIAN_POINT ( 'NONE',  ( -4.498618707852113374, 2.988074248075567318, -0.6999999999999992895 ) ) ;
#23279=CARTESIAN_POINT ( 'NONE',  ( -3.885731905334995684, 2.027028853511404272, -0.9187643563000024161 ) ) ;
#23284=CARTESIAN_POINT ( 'NONE',  ( -5.853056545089267537, 1.703994407032248581, -16.90443125760000243 ) ) ;
#23285=CARTESIAN_POINT ( 'NONE',  ( -4.976668802704899086, 3.592974922927941073, -33.86696136360001219 ) ) ;
#23301=CARTESIAN_POINT ( 'NONE',  ( 1.270994686748740277, -4.981061367834454856, -0.7000029814077138868 ) ) ;
#23324=CARTESIAN_POINT ( 'NONE',  ( -3.866727543631055308, 3.949224786475222349, -5.568732180600000525 ) ) ;
#23325=CARTESIAN_POINT ( 'NONE',  ( -5.611385130160316592, 1.726552310816597435, -21.32289663400000634 ) ) ;
#23345=CARTESIAN_POINT ( 'NONE',  ( 4.725722714896615884, -3.873618144318392797, -23.99674734060000603 ) ) ;
#23371=CARTESIAN_POINT ( 'NONE',  ( 3.550610403408205329, -5.007233058897099021, -11.52388893670000591 ) ) ;
#23431=CARTESIAN_POINT ( 'NONE',  ( 5.672553144689285176, -0.9485505809898806540, -36.34517599849999669 ) ) ;
#23432=VERTEX_POINT ( 'NONE', #18517 ) ;
#23447=CARTESIAN_POINT ( 'NONE',  ( -3.052679639724400928, 3.117809041995142749, -4.568732180599999637 ) ) ;
#23451=CARTESIAN_POINT ( 'NONE',  ( -2.579713781069702616, -4.412685520613435664, -16.61932079290000530 ) ) ;
#23452=CARTESIAN_POINT ( 'NONE',  ( 4.373195337096333013, -2.904765488536246387, -35.35875473020000470 ) ) ;
#23464=( NAMED_UNIT ( * ) SI_UNIT ( $, .STERADIAN. ) SOLID_ANGLE_UNIT ( ) );
#23465=CARTESIAN_POINT ( 'NONE',  ( -2.023360855367876354, -4.853169170121535814, -0.7001634333184084680 ) ) ;
#23484=CARTESIAN_POINT ( 'NONE',  ( -4.273751495587445604, 4.364932658710685587, -4.568732180600005854 ) ) ;
#23485=CARTESIAN_POINT ( 'NONE',  ( 0.3233900739386466605, 6.101867874933233793, -22.94418644579999977 ) ) ;
#23504=PLANE ( 'NONE',  #12306 ) ;
#23527=CARTESIAN_POINT ( 'NONE',  ( 3.665953941183818010, 4.858601989977915814, -13.62796858839999992 ) ) ;
#23601=CARTESIAN_POINT ( 'NONE',  ( -5.082228009654736312, -3.365126390422853220, -6.289929326000004650 ) ) ;
#23605=CARTESIAN_POINT ( 'NONE',  ( 4.130711734062741947, 1.221343755424970201, -18.04190840230000958 ) ) ;
#23621=CARTESIAN_POINT ( 'NONE',  ( -0.8383234616028363284, -5.156720310874200131, -0.7000226318098609068 ) ) ;
#23633=CARTESIAN_POINT ( 'NONE',  ( 3.235226967573094914, 2.011182562232342708, -35.69999999999999574 ) ) ;
#23639=CARTESIAN_POINT ( 'NONE',  ( 1.765446408317208560, -4.831419061753667421, -7.198085232199999517 ) ) ;
#23640=CARTESIAN_POINT ( 'NONE',  ( 1.566980368899947962, 4.067530462867743779, -26.09462237480000724 ) ) ;
#23657=CARTESIAN_POINT ( 'NONE',  ( -4.901082056042067592, -4.330235462241937228, -33.83447003409999354 ) ) ;
#23674=CARTESIAN_POINT ( 'NONE',  ( 3.718425205896203067, -3.001845489190030136, -0.7000011950963532792 ) ) ;
#23678=CARTESIAN_POINT ( 'NONE',  ( 3.390625094264292372, -3.362288366427768072, -14.12362212869999745 ) ) ;
#23736=CARTESIAN_POINT ( 'NONE',  ( 4.457006042266220547, -0.7452897422089094226, -36.68267599850000238 ) ) ;
#23752=CARTESIAN_POINT ( 'NONE',  ( 1.604951280288043014, -4.392199147046020435, -6.260585232200001293 ) ) ;
#23756=CARTESIAN_POINT ( 'NONE',  ( 4.180014548479816128, -1.737364395512316362, -18.80872516810000405 ) ) ;
#23784=CARTESIAN_POINT ( 'NONE',  ( 1.210976328703774474, 4.719380953081087959, -35.69999999999999574 ) ) ;
#23790=CARTESIAN_POINT ( 'NONE',  ( -2.150134890876696847, -3.785840986416655340, -6.685065142700001850 ) ) ;
#23791=CARTESIAN_POINT ( 'NONE',  ( 3.430850994441077439, -5.010772104901466406, -27.13292313650000764 ) ) ;
#23797=CARTESIAN_POINT ( 'NONE',  ( -3.679974273075529823, -2.251605409995534490, -21.90799200640000777 ) ) ;
#23832=CARTESIAN_POINT ( 'NONE',  ( 2.558869066659682723, 3.716983018758990287, -16.27509163649999735 ) ) ;
#23896=CARTESIAN_POINT ( 'NONE',  ( 4.198532171030673332, 1.238783022246746413, -35.53159726780000227 ) ) ;
#23912=CARTESIAN_POINT ( 'NONE',  ( 2.521631941452523229, 3.946033397249450125, -5.200967428500000267 ) ) ;
#23917=CARTESIAN_POINT ( 'NONE',  ( 4.790228392454985773, 0.1193559191107074896, -21.61411200059999871 ) ) ;
#23944=CARTESIAN_POINT ( 'NONE',  ( 0.5582180380177076406, 4.216789577812869005, -35.70000000000000284 ) ) ;
#23949=CARTESIAN_POINT ( 'NONE',  ( -2.823270949701056409, -2.499023824075683020, -0.6999999999999992895 ) ) ;
#23953=CARTESIAN_POINT ( 'NONE',  ( 0.1708583496781435063, 4.358252033550405358, -7.937690181100000686 ) ) ;
#23954=CARTESIAN_POINT ( 'NONE',  ( 4.370697773661016861, 1.580342671372844787, -26.51249766020000109 ) ) ;
#23959=CARTESIAN_POINT ( 'NONE',  ( -3.885731905334990799, 2.027028853511393613, -1.418764356299999418 ) ) ;
#23963=VERTEX_POINT ( 'NONE', #20380 ) ;
#23985=CARTESIAN_POINT ( 'NONE',  ( 0.7420639427752478978, -6.011517603930927045, -17.77054674910000287 ) ) ;
#24012=CARTESIAN_POINT ( 'NONE',  ( -1.151230282303595587, -4.494053275198272246, -28.04882611460000064 ) ) ;
#24023=CARTESIAN_POINT ( 'NONE',  ( 3.900999017799251956, -2.591123067748548614, -35.07256796030007706 ) ) ;
#24058=CARTESIAN_POINT ( 'NONE',  ( 2.246931792404676997, -6.149078805876593279, -5.660585232200005201 ) ) ;
#24064=CARTESIAN_POINT ( 'NONE',  ( -2.618143654921853969, 3.481518582925489991, -20.13064294429999990 ) ) ;
#24077=CARTESIAN_POINT ( 'NONE',  ( 4.420334067734101424, -4.199682076162645217, -30.05126389020000488 ) ) ;
#24091=CARTESIAN_POINT ( 'NONE',  ( 0.7747757076663149833, 4.116528746048892629, -35.69999999999999574 ) ) ;
#24099=CARTESIAN_POINT ( 'NONE',  ( 5.067327387632984959, 4.072231104569050686, -8.954586408000002606 ) ) ;
#24100=CARTESIAN_POINT ( 'NONE',  ( -3.052438874386679046, 3.509528713898351970, -28.08728588870000209 ) ) ;
#24106=CARTESIAN_POINT ( 'NONE',  ( -1.831588579526997940, 3.958388136463042439, -7.731725184300007214 ) ) ;
#24131=CARTESIAN_POINT ( 'NONE',  ( 2.479820170275052860, -4.407201367387826529, -0.7000592809870032074 ) ) ;
#24135=CARTESIAN_POINT ( 'NONE',  ( 4.130711734062741947, 1.221343755424970201, -17.04190840230000248 ) ) ;
#24158=CARTESIAN_POINT ( 'NONE',  ( -3.834000099192893973, 2.652495916366584439, -25.46779765530001072 ) ) ;
#24202=CARTESIAN_POINT ( 'NONE',  ( 1.765446408317208560, -4.831419061753667421, -5.323085232199998629 ) ) ;
#24208=CARTESIAN_POINT ( 'NONE',  ( 3.800013225884300905, -1.579422177728472487, -18.37122516810000050 ) ) ;
#24222=CARTESIAN_POINT ( 'NONE',  ( 3.157381476932438868, -2.999772911539577702, -30.05126389020000488 ) ) ;
#24235=CARTESIAN_POINT ( 'NONE',  ( 0.2030058330167056890, 4.518950146840584381, -35.69999999999999574 ) ) ;
#24243=CARTESIAN_POINT ( 'NONE',  ( -3.409041349409528632, -3.412796932024714014, -10.75149163099999505 ) ) ;
#24244=CARTESIAN_POINT ( 'NONE',  ( 0.6752547517502489605, 4.742883336923179094, -28.06850711719999936 ) ) ;
#24249=CARTESIAN_POINT ( 'NONE',  ( -2.618143654921863295, 3.481518582925488658, -19.63064294430000345 ) ) ;
#24280=CARTESIAN_POINT ( 'NONE',  ( -4.706847372945446750, -0.8873292358359263776, -15.16199426529999705 ) ) ;
#24308=CARTESIAN_POINT ( 'NONE',  ( -5.340187987486594068, -1.400932219821331870, -26.04656121680001135 ) ) ;
#24332=CARTESIAN_POINT ( 'NONE',  ( 3.653275382406361071, -2.426579979385206531, -0.6999999999999992895 ) ) ;
#24360=CARTESIAN_POINT ( 'NONE',  ( 3.904508939291349900, -1.994718106397494362, -11.41474735220000625 ) ) ;
#24366=CARTESIAN_POINT ( 'NONE',  ( 2.949882002856666130, 3.605460750137340131, -20.75622222230001057 ) ) ;
#24384=CARTESIAN_POINT ( 'NONE',  ( -4.273414424137721213, 4.913340199448848367, -28.58728588869999143 ) ) ;
#24399=CARTESIAN_POINT ( 'NONE',  ( 0.3172472662966961954, 4.344971966744158642, -35.70000000000000284 ) ) ;
#24405=CARTESIAN_POINT ( 'NONE',  ( -5.680091681631305178, 1.608645723366325164, -8.310827254900006622 ) ) ;
#24406=CARTESIAN_POINT ( 'NONE',  ( 5.869757812515316253, 0.5877190740209992104, -28.63116556699999649 ) ) ;
#24414=CARTESIAN_POINT ( 'NONE',  ( -0.7560282158644084927, 4.289996408053712962, -19.83583244400000112 ) ) ;
#24444=CARTESIAN_POINT ( 'NONE',  ( 0.6713911862884133219, -5.438992117826878747, -17.37054674910000074 ) ) ;
#24470=CARTESIAN_POINT ( 'NONE',  ( 5.307277461537168506, -2.951504967840870464, -26.93037294500000201 ) ) ;
#24486=CARTESIAN_POINT ( 'NONE',  ( 3.361768113024335758, -2.599356797695480115, -0.6999999999999992895 ) ) ;
#24515=CARTESIAN_POINT ( 'NONE',  ( 0.3624384587677526026, -4.645391411234340850, -9.393384211799999051 ) ) ;
#24521=CARTESIAN_POINT ( 'NONE',  ( -2.618143654921863295, 3.481518582925488658, -19.63064294430000345 ) ) ;
#24535=CARTESIAN_POINT ( 'NONE',  ( -6.085238278930475531, -0.01014600953121863602, -28.16856466009999593 ) ) ;
#24553=CARTESIAN_POINT ( 'NONE',  ( -3.737088657310626338, 2.230226196412739892, -0.6999999999999992895 ) ) ;
#24554=CARTESIAN_POINT ( 'NONE',  ( 0.6465148687819723961, -4.727082501359223699, 0.5643759519999985708 ) ) ;
#24558=CARTESIAN_POINT ( 'NONE',  ( 0.3624384587677526026, -4.645391411234340850, -9.393384211799999051 ) ) ;
#24559=CARTESIAN_POINT ( 'NONE',  ( 1.882647771056453756, 3.960165260869607629, -31.65113063600000487 ) ) ;
#24597=CARTESIAN_POINT ( 'NONE',  ( -2.554946692801202346, -3.999086378171832212, -20.77141267860000795 ) ) ;
#24620=CARTESIAN_POINT ( 'NONE',  ( 3.430850994441077439, -5.010772104901466406, -27.13292313650000764 ) ) ;
#24639=CARTESIAN_POINT ( 'NONE',  ( 3.119449978080022667, -2.770394852667431351, -0.6999999999999992895 ) ) ;
#24672=CARTESIAN_POINT ( 'NONE',  ( -4.047971700345533996, -2.476765951014430200, -22.84549200639999711 ) ) ;
#24685=CARTESIAN_POINT ( 'NONE',  ( -3.357682761866084498, 3.860481585313637609, -29.52478588869999854 ) ) ;
#24702=CARTESIAN_POINT ( 'NONE',  ( -4.895789606679002759, -1.770905548711505295, -0.6999999999999992895 ) ) ;
#24705=CARTESIAN_POINT ( 'NONE',  ( -5.527020701484460119, 0.1640065206915941320, -14.18304957890000040 ) ) ;
#24706=CARTESIAN_POINT ( 'NONE',  ( -5.984522419796141079, -1.167122196978044535, -31.09652066320001040 ) ) ;
#24714=CARTESIAN_POINT ( 'NONE',  ( -4.339197174995631734, 0.6278332542688225271, -34.25783976329999092 ) ) ;
#24741=PRODUCT ( 'Drive Spring', 'Drive Spring', '', ( #25315 ) ) ;
#24746=CARTESIAN_POINT ( 'NONE',  ( 4.129834804009608007, 5.047645050193429128, -19.65622222229999849 ) ) ;
#24792=CARTESIAN_POINT ( 'NONE',  ( -2.017871889752692383, -3.161030873707806332, -0.6999999999999992895 ) ) ;
#24823=ORIENTED_EDGE ( 'NONE', *, *, #1054, .F. ) ;
#24828=CARTESIAN_POINT ( 'NONE',  ( 0.2309929099465236890, 4.358477053493579056, -23.44418644580000333 ) ) ;
#24845=CARTESIAN_POINT ( 'NONE',  ( -3.500772897184941446, -3.093025330206539802, -34.33447003410000775 ) ) ;
#24863=CARTESIAN_POINT ( 'NONE',  ( -4.140124079000881530, 2.264562353281220908, -0.6999999999999992895 ) ) ;
#24869=CARTESIAN_POINT ( 'NONE',  ( -4.992376002455611861, -2.377191163393747253, -13.97655742010000779 ) ) ;
#24870=CARTESIAN_POINT ( 'NONE',  ( -4.274658871253798509, -0.8336587121505270037, -31.09652066320001040 ) ) ;
#24874=CARTESIAN_POINT ( 'NONE',  ( -3.878879136156893281, -1.961445906012333706, -27.96472909260000606 ) ) ;
#24905=CARTESIAN_POINT ( 'NONE',  ( 0.8228371056950706253, -6.016286819831330845, -0.3731240480000022619 ) ) ;
#24906=CARTESIAN_POINT ( 'NONE',  ( 1.265035515811500089, -4.453021097817299712, -20.79535708920001014 ) ) ;
#24934=PRESENTATION_STYLE_ASSIGNMENT (( #720 ) ) ;
#24945=CARTESIAN_POINT ( 'NONE',  ( 3.357972723926252456, -2.601985670799683348, -0.6999999999999992895 ) ) ;
#24976=CARTESIAN_POINT ( 'NONE',  ( 4.692682656939434871, -1.014318600726540787, -24.72786215649999519 ) ) ;
#24990=CARTESIAN_POINT ( 'NONE',  ( 2.635706879431563898, 5.544231365240147369, -32.75113063600000629 ) ) ;
#25004=CARTESIAN_POINT ( 'NONE',  ( 3.242686849810665795, 3.944686721199032853, -35.69999999999999574 ) ) ;
#25007=CARTESIAN_POINT ( 'NONE',  ( -3.793660607282320463, 2.420557939024130967, -0.6999999999999991784 ) ) ;
#25013=CARTESIAN_POINT ( 'NONE',  ( -0.6370991518874399295, 4.292107257743936977, -11.36772091660000150 ) ) ;
#25014=CARTESIAN_POINT ( 'NONE',  ( 4.904813032679735230, 3.691647504909488564, -31.76032172560000433 ) ) ;
#25021=CARTESIAN_POINT ( 'NONE',  ( 3.802779202691175531, 1.094990851247104491, -35.53910482769999390 ) ) ;
#25053=CARTESIAN_POINT ( 'NONE',  ( -5.478535709405480958, -2.209361269785813153, -1.997197434499998758 ) ) ;
#25054=CARTESIAN_POINT ( 'NONE',  ( -4.448701673712592175, 0.6187532242676700989, -18.75159460730000660 ) ) ;
#25069=CARTESIAN_POINT ( 'NONE',  ( -2.564224011391953884, 5.541743391097003979, -7.731725184300000997 ) ) ;
#25093=CARTESIAN_POINT ( 'NONE',  ( -4.338779899226326009, -4.343559731693466652, -9.213991631000000737 ) ) ;
#25133=CARTESIAN_POINT ( 'NONE',  ( 3.375516224911112584, -2.766870103071181308, -23.99674734060000603 ) ) ;
#25146=CARTESIAN_POINT ( 'NONE',  ( -0.4593365651765490831, 6.553622599173768215, -34.89518930509999706 ) ) ;
#25157=EDGE_LOOP ( 'NONE', ( #5824, #10751, #18844, #15546, #14327, #9473 ) ) ;
#25164=CARTESIAN_POINT ( 'NONE',  ( -5.045264861105531295, 0.3129595611791647913, -0.6999999999999992895 ) ) ;
#25165=CARTESIAN_POINT ( 'NONE',  ( 4.360957369889332469, -0.1505632777267530420, -2.185409721200005428 ) ) ;
#25169=CARTESIAN_POINT ( 'NONE',  ( 4.294959833232216972, -2.194189917041240445, -12.85224735220000092 ) ) ;
#25170=CARTESIAN_POINT ( 'NONE',  ( -2.539202180960155264, -4.449342792696782567, -29.73892233980000910 ) ) ;
#25205=CARTESIAN_POINT ( 'NONE',  ( -3.510061880997908279, 5.032561185093348044, -1.627651354100000169 ) ) ;
#25206=CARTESIAN_POINT ( 'NONE',  ( -0.8316310374238428116, 4.718996048841939128, -18.89833244400000822 ) ) ;
#25226=CARTESIAN_POINT ( 'NONE',  ( 5.067327387632984959, 4.072231104569050686, -8.354586407999999409 ) ) ;
#25243=APPLICATION_CONTEXT ( 'automotive_design' ) ;
#25250=CARTESIAN_POINT ( 'NONE',  ( 3.619519562537643065, 2.908736503316577959, -8.354586408000006514 ) ) ;
#25269=SURFACE_STYLE_FILL_AREA ( #8572 ) ;
#25297=ADVANCED_BREP_SHAPE_REPRESENTATION ( '', ( #890, #17722 ), #11232 ) ;
#25308=CARTESIAN_POINT ( 'NONE',  ( 3.503437880484509659, 2.636891074944046398, -32.36032172559999509 ) ) ;
#25315=PRODUCT_CONTEXT ( 'NONE', #25243, 'mechanical' ) ;
#25324=CARTESIAN_POINT ( 'NONE',  ( -2.507187057889194381, 3.594686560818127763, -1.627651354100000169 ) ) ;
#25328=CARTESIAN_POINT ( 'NONE',  ( -2.929853409778804263, 3.622264489389753539, -14.10352819870000829 ) ) ;
#25350=CARTESIAN_POINT ( 'NONE',  ( -0.08587345398629391002, -5.205186680070521987, -0.7000563607978648184 ) ) ;
#25372=CARTESIAN_POINT ( 'NONE',  ( 4.360957369889332469, -0.1505632777267530420, -3.185409721200004984 ) ) ;
#25373=CARTESIAN_POINT ( 'NONE',  ( 3.375516224911112584, -2.766870103071181308, -23.99674734060000603 ) ) ;
#25388=ORIENTED_EDGE ( 'NONE', *, *, #1054, .T. ) ;
#25391=CARTESIAN_POINT ( 'NONE',  ( -3.360743903619262340, -4.083497937754941631, -0.7578093794999990473 ) ) ;
#25416=CARTESIAN_POINT ( 'NONE',  ( 4.310466091822801715, 1.786666325167806546, -10.99261350020000982 ) ) ;
#25471=CARTESIAN_POINT ( 'NONE',  ( 0.09516252086846690994, -5.505278045713965618, -34.41110030500000505 ) ) ;
#25486=CARTESIAN_POINT ( 'NONE',  ( 1.334940606749785319, 4.973974987606708531, -1.115910702900006601 ) ) ;
#25489=CARTESIAN_POINT ( 'NONE',  ( -4.706847372945446750, -0.8873292358359263776, -17.03699426529999883 ) ) ;
#25490=CARTESIAN_POINT ( 'NONE',  ( -6.074876045044606876, 0.8789665559579967757, -33.65783976330000371 ) ) ;
#25496=EDGE_CURVE ( 'NONE', #21685, #23963, #15946, .T. ) ;
#25500=ADVANCED_FACE ( 'NONE', ( #28204 ), #23504, .F. ) ;
#25508=CARTESIAN_POINT ( 'NONE',  ( -0.7723098159415937580, -5.165446492250387323, -0.7000230395128266281 ) ) ;
#25520=CARTESIAN_POINT ( 'NONE',  ( 3.163495726740022551, 2.135910292705673452, -35.69999999999998863 ) ) ;
#25527=CARTESIAN_POINT ( 'NONE',  ( -6.505526340832360255, -0.4164809035307331930, -4.148838774900000637 ) ) ;
#25528=CARTESIAN_POINT ( 'NONE',  ( -3.579388909039125988, -3.189794392837340009, -23.90351932450001016 ) ) ;
#25536=CARTESIAN_POINT ( 'NONE',  ( -2.746723693872569871, -2.614252338060372161, -0.8157167102000040249 ) ) ;
#25545=CARTESIAN_POINT ( 'NONE',  ( -1.814319851916122772, 5.833166587536846137, -4.774955258300003891 ) ) ;
#25563=CARTESIAN_POINT ( 'NONE',  ( 4.799848611324305736, -2.144583235354477591, -35.69999999999999574 ) ) ;
#25568=CARTESIAN_POINT ( 'NONE',  ( 2.618538529469180531, 3.470429992801026042, -14.22796858840000311 ) ) ;
#25608=( BOUNDED_CURVE ( )  B_SPLINE_CURVE ( 5, ( #10972, #5776, #13480, #13643, #3727, #10819 ),
 .UNSPECIFIED., .F., .F. ) 
 B_SPLINE_CURVE_WITH_KNOTS ( ( 6, 6 ),
 ( 11.42265871740000094, 12.17014935140000098 ),
 .UNSPECIFIED. ) 
 CURVE ( )  GEOMETRIC_REPRESENTATION_ITEM ( )  RATIONAL_B_SPLINE_CURVE ( ( 0.3231753219119999909, 0.3307207062469999514, 0.3388331752689999754, 0.3475394025169999956, 0.3568692924569999980, 0.3668559804790000323 ) ) 
 REPRESENTATION_ITEM ( '' )  );
#25634=CARTESIAN_POINT ( 'NONE',  ( 5.672553144689285176, -0.9485505809898806540, -35.74517599850000948 ) ) ;
#25649=CARTESIAN_POINT ( 'NONE',  ( -2.757905763689965095, 3.954155216896602987, -0.6901513540999957286 ) ) ;
#25653=CARTESIAN_POINT ( 'NONE',  ( 4.315341029122434335, -4.279276102762477940, -15.06112212870000455 ) ) ;
#25654=CARTESIAN_POINT ( 'NONE',  ( -4.976668802704899086, 3.592974922927941073, -34.46696136359999940 ) ) ;
#25688=CARTESIAN_POINT ( 'NONE',  ( -2.886686092853935293, -3.810306705960904594, -4.666445369299999868 ) ) ;
#25689=CARTESIAN_POINT ( 'NONE',  ( -5.902313038799129608, -1.548398769286710053, -25.04656121680000425 ) ) ;
#25705=CARTESIAN_POINT ( 'NONE',  ( 0.1051796283266584475, -6.084780997910130829, -33.41110030499999795 ) ) ;
#25726=CARTESIAN_POINT ( 'NONE',  ( -4.101794773660127902, 5.071170285176791914, -13.00352819870000154 ) ) ;
#25801=CARTESIAN_POINT ( 'NONE',  ( -4.274305095845718938, 2.229731738857087642, -0.4812643562999985303 ) ) ;
#25807=CARTESIAN_POINT ( 'NONE',  ( -4.180754675048095947, 1.217138862148074763, -16.30443125759999745 ) ) ;
#25808=CARTESIAN_POINT ( 'NONE',  ( -6.074876045044606876, 0.8789665559579967757, -34.25783976329999092 ) ) ;
#25823=CARTESIAN_POINT ( 'NONE',  ( 0.9172539291170586084, -5.086450260305231730, -0.6999820721555671810 ) ) ;
#25835=CARTESIAN_POINT ( 'NONE',  ( 3.009918263491472512, 2.374761854523940396, -35.69999999999999574 ) ) ;
#25843=CARTESIAN_POINT ( 'NONE',  ( -0.8661127261961210078, -4.701195862525644031, -4.462734013000006605 ) ) ;
#25844=CARTESIAN_POINT ( 'NONE',  ( -2.496099253731141943, 5.577352528212363048, -22.13780126169999463 ) ) ;
#25861=CARTESIAN_POINT ( 'NONE',  ( -5.864216825196034932, 1.669623860970033347, -31.30158078969999380 ) ) ;
#25883=CARTESIAN_POINT ( 'NONE',  ( 3.082386449366550263, -3.056625787687238471, -15.06112212870000455 ) ) ;
#25935=CARTESIAN_POINT ( 'NONE',  ( 4.198532171036193361, 1.238783022255082189, -36.03159726780002359 ) ) ;
#25952=CARTESIAN_POINT ( 'NONE',  ( 6.086077541567210147, 0.7980478301550381071, -5.026979598399996974 ) ) ;
#25957=CARTESIAN_POINT ( 'NONE',  ( 5.232234863148874204, 1.547035423556993639, -18.54190840230001314 ) ) ;
#25958=CARTESIAN_POINT ( 'NONE',  ( -3.554763430470067043, 2.566410659217312151, -33.96696136360001361 ) ) ;
#25973=( NAMED_UNIT ( * ) PLANE_ANGLE_UNIT ( ) SI_UNIT ( $, .RADIAN. ) );
#25986=CARTESIAN_POINT ( 'NONE',  ( 3.759125770765979535, 0.1161620079115446708, -35.69999999999999574 ) ) ;
#25989=CARTESIAN_POINT ( 'NONE',  ( 3.843630909669756957, -2.553018000905745044, -0.6999999999999992895 ) ) ;
#25993=CARTESIAN_POINT ( 'NONE',  ( 2.246931792404676997, -6.149078805876593279, -6.860585232200004491 ) ) ;
#25994=CARTESIAN_POINT ( 'NONE',  ( -0.6320852424383932577, 6.069672320066970883, -25.28903409330000684 ) ) ;
#26010=CARTESIAN_POINT ( 'NONE',  ( -4.976668802705447092, 3.592974922927108405, -34.46696136359999940 ) ) ;
#26030=CARTESIAN_POINT ( 'NONE',  ( 3.170293664407711098, -3.797356553874626783, -0.6999183984185574081 ) ) ;
#26034=CARTESIAN_POINT ( 'NONE',  ( 2.880392382415891017, 3.817472992077249661, -13.29046858840000311 ) ) ;
#26107=CARTESIAN_POINT ( 'NONE',  ( -2.150134890876696847, -3.785840986416655340, -6.185065142700006291 ) ) ;
#26111=CARTESIAN_POINT ( 'NONE',  ( -4.180754675048084401, 1.217138862148065659, -16.80443125760001521 ) ) ;
#26142=CARTESIAN_POINT ( 'NONE',  ( 0.2315610464403904389, 4.417977769816408440, -35.69999999999999574 ) ) ;
#26148=CARTESIAN_POINT ( 'NONE',  ( -3.010188847181571870, -5.300177381000955812, -7.285065142700005048 ) ) ;
#26149=CARTESIAN_POINT ( 'NONE',  ( 2.450607853129164848, -3.579122932049590755, -27.13292313650000764 ) ) ;
#26154=CARTESIAN_POINT ( 'NONE',  ( 2.949882002856674124, 3.605460750137338799, -20.25622222230000347 ) ) ;
#26162=CARTESIAN_POINT ( 'NONE',  ( -2.705882613314523955, 5.963358562559473164, -31.72635571290000200 ) ) ;
#26179=CARTESIAN_POINT ( 'NONE',  ( 3.226399722048018948, -3.735024872883826674, -0.6998763472199169833 ) ) ;
#26184=CARTESIAN_POINT ( 'NONE',  ( -4.363437395929419260, 0.1294788321584625090, -13.18304957890000573 ) ) ;
#26258=CARTESIAN_POINT ( 'NONE',  ( -2.723504195107721237, -4.795398582787750108, -5.685065142700003626 ) ) ;
#26262=CARTESIAN_POINT ( 'NONE',  ( 2.949882002856674124, 3.605460750137338799, -20.25622222230000347 ) ) ;
#26291=CARTESIAN_POINT ( 'NONE',  ( 0.5114632729423386204, 4.239061013832984948, -35.69999999999999574 ) ) ;
#26298=CARTESIAN_POINT ( 'NONE',  ( 0.1708583496781539146, 4.358252033550397364, -8.437690181099997133 ) ) ;
#26299=CARTESIAN_POINT ( 'NONE',  ( 5.307277461537168506, -2.951504967840870464, -26.33037294500000058 ) ) ;
#26305=CARTESIAN_POINT ( 'NONE',  ( 2.618538529469180531, 3.470429992801026042, -14.22796858840000311 ) ) ;
#26317=CARTESIAN_POINT ( 'NONE',  ( -6.085238278930475531, -0.01014600953121863602, -28.16856466009999593 ) ) ;
#26337=CARTESIAN_POINT ( 'NONE',  ( 3.538401481699890994, -3.323650355412237190, -0.6997877701626019631 ) ) ;
#26341=CARTESIAN_POINT ( 'NONE',  ( 4.543782907447139863, 1.343478130985185537, -16.60440840229999893 ) ) ;
#26370=CARTESIAN_POINT ( 'NONE',  ( 3.430850994441077439, -5.010772104901466406, -27.73292313649999841 ) ) ;
#26386=CARTESIAN_POINT ( 'NONE',  ( 3.269803491262430306, -2.171870132384594587, -35.34814375549996157 ) ) ;
#26416=CARTESIAN_POINT ( 'NONE',  ( 4.116710911288352648, -1.508563155650267884, -5.836105321700007842 ) ) ;
#26421=CARTESIAN_POINT ( 'NONE',  ( 0.5830502407437251344, -4.723335260236232180, -19.30804674910000784 ) ) ;
#26434=CARTESIAN_POINT ( 'NONE',  ( -3.052438874386664835, 3.509528713898347974, -28.58728588869999143 ) ) ;
#26448=CARTESIAN_POINT ( 'NONE',  ( 0.4968125066838017245, 4.681645040665504354, -35.70000000000000284 ) ) ;
#26455=CARTESIAN_POINT ( 'NONE',  ( -5.530047734074942767, 3.478668956039820959, -11.04547590279999980 ) ) ;
#26456=CARTESIAN_POINT ( 'NONE',  ( 3.104103280670445830, -4.533555713950848443, -26.13292313650000409 ) ) ;
#26462=CARTESIAN_POINT ( 'NONE',  ( -4.448701673712585070, 0.6187532242676665462, -19.25159460730001371 ) ) ;
#26485=CARTESIAN_POINT ( 'NONE',  ( 2.715726573628606477, -4.227879611059382370, -0.6999936726990061420 ) ) ;
#26489=CARTESIAN_POINT ( 'NONE',  ( 4.130711734062736618, 1.221343755424965316, -17.54190840230000248 ) ) ;
#26498=PLANE ( 'NONE',  #9683 ) ;
#26516=CARTESIAN_POINT ( 'NONE',  ( -4.215937884789293655, -1.105999120962562809, -25.04656121680000425 ) ) ;
#26564=CARTESIAN_POINT ( 'NONE',  ( -2.564224011386423641, 5.541743391105337757, -7.131725184300004017 ) ) ;
#26570=CARTESIAN_POINT ( 'NONE',  ( 6.096654317658788180, 0.1519075334363156893, -20.67661200060000226 ) ) ;
#26585=CARTESIAN_POINT ( 'NONE',  ( 4.634019325638262465, 0.4639887426745106791, -29.63116556699998938 ) ) ;
#26601=CARTESIAN_POINT ( 'NONE',  ( 0.5561711591857212422, 4.217760595753933472, -35.69999999999999574 ) ) ;
#26607=CARTESIAN_POINT ( 'NONE',  ( 0.3624384587677549341, -4.645391411234346180, -9.893384211800000827 ) ) ;
#26608=CARTESIAN_POINT ( 'NONE',  ( -6.085238278930475531, -0.01014600953121863602, -27.56856466010000517 ) ) ;
#26613=CARTESIAN_POINT ( 'NONE',  ( -3.099128499470596321, -3.102542665468454253, -9.813991631000003935 ) ) ;
#26644=CARTESIAN_POINT ( 'NONE',  ( -5.853056545089267537, 1.703994407032248581, -15.70443125760000136 ) ) ;
#26666=CARTESIAN_POINT ( 'NONE',  ( -3.579388909039125988, -3.189794392837340009, -25.77851932450001016 ) ) ;
#26713=CARTESIAN_POINT ( 'NONE',  ( 0.4590887144193210312, -5.884162454197269909, -8.393384211800002603 ) ) ;
#26718=CARTESIAN_POINT ( 'NONE',  ( -2.449727287106972184, -3.823908298404834483, -19.64294088819999828 ) ) ;
#26732=CARTESIAN_POINT ( 'NONE',  ( -5.984522419796141079, -1.167122196978044535, -31.09652066320001040 ) ) ;
#26749=CARTESIAN_POINT ( 'NONE',  ( 0.5919590525021038996, 4.200897578713889580, -35.69999999999999574 ) ) ;
#26757=CARTESIAN_POINT ( 'NONE',  ( -1.831588579526983063, 3.958388136463033558, -8.231725184300008991 ) ) ;
#26758=CARTESIAN_POINT ( 'NONE',  ( 2.450607853129171954, -3.579122932049592976, -26.63292313650000764 ) ) ;
#26765=CARTESIAN_POINT ( 'NONE',  ( -4.484282906631567478, 1.269983465873030015, -7.310827254900003069 ) ) ;
#26794=CARTESIAN_POINT ( 'NONE',  ( 2.992916622598570608, -2.824380467281231599, -17.53565261000000319 ) ) ;
#26822=CARTESIAN_POINT ( 'NONE',  ( -0.5718866478877175918, 5.491608289559616551, -26.88903409329999761 ) ) ;
#26834=AXIS2_PLACEMENT_3D ( 'NONE', #23254, #6409, #21199 ) ;
#26841=CARTESIAN_POINT ( 'NONE',  ( 3.048238659810818429, -2.820297993983834406, -0.6999999999999991784 ) ) ;
#26854=( LENGTH_UNIT ( ) NAMED_UNIT ( * ) SI_UNIT ( .MILLI., .METRE. ) );
#26872=CARTESIAN_POINT ( 'NONE',  ( 4.689100480956518879, -0.8300439969826994835, -7.833982634700003445 ) ) ;
#26879=CARTESIAN_POINT ( 'NONE',  ( 0.5300456733980246637, -4.293941145674104121, -18.37054674910000429 ) ) ;
#26894=CARTESIAN_POINT ( 'NONE',  ( -2.308365619037855421, -4.044857084274065429, -30.67642233980000199 ) ) ;
#26914=CARTESIAN_POINT ( 'NONE',  ( 2.816286225276055433, -4.345042730952153320, 0.8340606117000020081 ) ) ;
#26917=CARTESIAN_POINT ( 'NONE',  ( 4.584724779240096915, 3.684399570836669024, -9.354586408000001185 ) ) ;
#26918=CARTESIAN_POINT ( 'NONE',  ( 6.487627055914963137, 0.6495842397260740420, -29.63116556699998938 ) ) ;
#26953=LINE ( 'NONE', #31096, #15430 ) ;
#26954=CARTESIAN_POINT ( 'NONE',  ( -4.047971700351067348, -2.476765951022760870, -20.97049200639999356 ) ) ;
#26978=CARTESIAN_POINT ( 'NONE',  ( 2.450607853129164848, -3.579122932049590755, -27.13292313650000764 ) ) ;
#26983=SURFACE_SIDE_STYLE ('',( #20059 ) ) ;
#26997=CARTESIAN_POINT ( 'NONE',  ( 1.770085743148440027, -3.528255691684338391, -0.6999999999999995115 ) ) ;
#27026=CARTESIAN_POINT ( 'NONE',  ( -3.950034095761360664, 2.484763540022561834, -9.945475902800005485 ) ) ;
#27031=CARTESIAN_POINT ( 'NONE',  ( -2.322678811625143780, -3.635533071076384015, -21.70891267860000795 ) ) ;
#27046=CARTESIAN_POINT ( 'NONE',  ( -4.188726303739433554, 1.192588472141202560, -31.30158078970000801 ) ) ;
#27059=CARTESIAN_POINT ( 'NONE',  ( 3.306876859848844941, 3.897974197644354266, -35.69999999999999574 ) ) ;
#27062=CARTESIAN_POINT ( 'NONE',  ( -5.096481347195676470, -0.2862171934127135109, -0.6999999999999991784 ) ) ;
#27066=CARTESIAN_POINT ( 'NONE',  ( 4.310466091822801715, 1.786666325167806546, -11.99261350020000272 ) ) ;
#27067=CARTESIAN_POINT ( 'NONE',  ( 3.157381476932436648, -2.999772911539579034, -29.55126389020000133 ) ) ;
#27075=CARTESIAN_POINT ( 'NONE',  ( 4.556810990865953315, -1.030009251744165688, -32.78377053309999667 ) ) ;
#27106=CARTESIAN_POINT ( 'NONE',  ( 4.373195337096347224, -2.904765488536225515, -0.5587547301999993277 ) ) ;
#27107=CARTESIAN_POINT ( 'NONE',  ( 3.931047123110473329, -1.876836795983962469, -20.88180150029999993 ) ) ;
#27153=CARTESIAN_POINT ( 'NONE',  ( -0.8663085823657415974, -3.674610306298811135, -0.6999999999999992895 ) ) ;
#27183=CARTESIAN_POINT ( 'NONE',  ( -3.251750336246070461, -5.089746299513510763, -22.30891267860000937 ) ) ;
#27199=CARTESIAN_POINT ( 'NONE',  ( 6.379535387291454640, -1.442012952481606991, -33.38377053310000520 ) ) ;
#27212=CARTESIAN_POINT ( 'NONE',  ( 1.669414676675136322, 4.650989935738711445, -35.69999999999999574 ) ) ;
#27215=CARTESIAN_POINT ( 'NONE',  ( -3.915568621502395708, 1.076153403323427682, -0.6999999999999992895 ) ) ;
#27216=CARTESIAN_POINT ( 'NONE',  ( 3.123710955063065065, -2.074832491810036039, 0.04124526979999709742 ) ) ;
#27219=CARTESIAN_POINT ( 'NONE',  ( 2.880392382415891017, 3.817472992077249661, -15.16546858840000489 ) ) ;
#27220=CARTESIAN_POINT ( 'NONE',  ( 2.039164074698236906, -5.746172002732055084, -29.65632401680000285 ) ) ;
#27257=CARTESIAN_POINT ( 'NONE',  ( 5.523879335194060936, -0.1907134851046367874, -3.685409721200002320 ) ) ;
#27258=CARTESIAN_POINT ( 'NONE',  ( 6.096654317658788180, 0.1519075334363156893, -20.07661200060000084 ) ) ;
#27272=CARTESIAN_POINT ( 'NONE',  ( -6.108812354261965005, 0.1812703649581512422, -13.18304957890000040 ) ) ;
#27292=B_SPLINE_CURVE_WITH_KNOTS ( 'NONE', 3,
 ( #13391, #25986, #18581, #16222, #6152, #15750, #28180, #23633, #25520, #25835, #20634, #4273, #27870, #11044, #3803, #1911, #21109, #9132, #11660, #4425, #18733, #6783, #2069, #18896, #23000, #1448, #6317, #30230, #4890, #14800, #12117, #21725, #14496, #21892, #9608, #24091, #16681, #28492, #2530, #26749, #12427, #11967, #23944, #493, #26601, #26291, #10078, #177, #7554, #9921, #31012, #7399, #19206, #24399, #16843, #28649, #9447, #16532, #26142, #9760, #21578, #6932, #24235, #19050, #28791, #25, #14649, #17144, #4735, #7249, #2833, #5040, #5186, #26448, #4575, #2382, #19367, #28957, #338, #16996, #2680, #22043, #7093, #11816, #14345, #14180, #19521, #23784, #12275, #29107, #2226, #21423, #17302, #27212, #5955, #3288, #12892, #5651, #13040, #794, #15105, #22343, #10384, #25004, #27059, #27365, #17747, #15249, #10537, #5807, #1252, #22801, #3437, #17604 ),
 .UNSPECIFIED., .F., .F.,
 ( 4, 2, 2, 2, 2, 1, 2, 2, 1, 1, 1, 2, 2, 1, 1, 1, 1, 1, 2, 2, 1, 1, 1, 2, 2, 1, 1, 1, 1, 2, 2, 1, 1, 1, 1, 2, 2, 1, 2, 2, 1, 2, 2, 1, 1, 1, 1, 2, 2, 1, 1, 2, 2, 1, 1, 2, 2, 1, 1, 2, 2, 1, 2, 2, 1, 1, 2, 2, 1, 2, 2, 2, 2, 2, 4 ),
 ( 0.000000000000000000, 0.06249999999999901468, 0.1249999999999980016, 0.1562499999999974742, 0.1874999999999969746, 0.2187499999999964473, 0.2343749999999961975, 0.2499999999999959477, 0.2812499999999953926, 0.2968749999999951150, 0.3046874999999949485, 0.3085937499999948930, 0.3124999999999947820, 0.3437499999999938938, 0.3593749999999935052, 0.3671874999999932832, 0.3710937499999931721, 0.3730468749999931166, 0.3740234374999931166, 0.3749999999999931166, 0.3906249999999933387, 0.3984374999999935052, 0.4023437499999935052, 0.4042968749999935052, 0.4062499999999935607, 0.4140624999999935052, 0.4179687499999935052, 0.4199218749999935607, 0.4208984374999935052, 0.4213867187499935607, 0.4218749999999936162, 0.4296874999999941158, 0.4335937499999943934, 0.4355468749999945599, 0.4365234374999946154, 0.4370117187499945599, 0.4374999999999945044, 0.4453124999999940048, 0.4462890624999938938, 0.4472656249999938383, 0.4492187499999936162, 0.4531249999999932276, 0.4570312499999928391, 0.4609374999999924505, 0.4648437499999920619, 0.4667968749999918399, 0.4677734374999917843, 0.4682617187499917288, 0.4687499999999916733, 0.4765624999999916733, 0.4804687499999916733, 0.4824218749999916733, 0.4843749999999916733, 0.4921874999999917288, 0.4960937499999917843, 0.4980468749999918399, 0.4999999999999918399, 0.5156249999999921174, 0.5234374999999922284, 0.5273437499999922284, 0.5312499999999923395, 0.5468749999999925615, 0.5546874999999927836, 0.5624999999999930056, 0.5937499999999937828, 0.6093749999999940048, 0.6171874999999941158, 0.6249999999999942268, 0.6562499999999947820, 0.6718749999999950040, 0.6874999999999951150, 0.7187499999999956701, 0.7499999999999961142, 0.8749999999999981126, 1.000000000000000000 ),
 .UNSPECIFIED. ) ;
#27338=CARTESIAN_POINT ( 'NONE',  ( 4.700333466414979178, 3.591691549163662511, -24.36727430110000370 ) ) ;
#27352=CARTESIAN_POINT ( 'NONE',  ( -0.3609073012553025150, 5.149274899367955349, -35.83268930509999706 ) ) ;
#27365=CARTESIAN_POINT ( 'NONE',  ( 3.491126794077959783, 3.756748552635288174, -35.70000000000000284 ) ) ;
#27370=CARTESIAN_POINT ( 'NONE',  ( -4.478443094736791252, 1.857700152298996210, -0.6999999999999994005 ) ) ;
#27376=CARTESIAN_POINT ( 'NONE',  ( 3.665953941183818010, 4.858601989977915814, -14.82796858839999921 ) ) ;
#27377=CARTESIAN_POINT ( 'NONE',  ( -3.231711866632715147, -5.662799918003592836, -30.07642233980000057 ) ) ;
#27382=CARTESIAN_POINT ( 'NONE',  ( 3.710789578725101734, 2.835545959904678170, -23.36727430110000014 ) ) ;
#27409=CARTESIAN_POINT ( 'NONE',  ( -4.325159770583737462, -1.744232581393518444, -0.9971974345000036433 ) ) ;
#27410=CARTESIAN_POINT ( 'NONE',  ( -3.316315296248301792, 4.409923538414076027, -18.63064294430000345 ) ) ;
#27422=CARTESIAN_POINT ( 'NONE',  ( 6.482330152203070739, 0.4632910120546396282, -14.64454535870000207 ) ) ;
#27460=EDGE_CURVE ( 'NONE', #7914, #29606, #25608, .T. ) ;
#27481=CARTESIAN_POINT ( 'NONE',  ( 5.972505199797514486, -1.290950946386169917, -23.79036215650000230 ) ) ;
#27496=CARTESIAN_POINT ( 'NONE',  ( -3.910239773549598397, 2.823051725158805425, -35.40446136359998519 ) ) ;
#27514=CARTESIAN_POINT ( 'NONE',  ( -3.762209872552725543, 2.386954303616800388, -0.6999999999999992895 ) ) ;
#27515=CARTESIAN_POINT ( 'NONE',  ( -1.763726019828893321, -5.203278105301040846, 0.4243694872999951850 ) ) ;
#27519=CARTESIAN_POINT ( 'NONE',  ( 4.310466091822805268, 1.786666325167808544, -11.49261350019999739 ) ) ;
#27520=CARTESIAN_POINT ( 'NONE',  ( 0.07512830594655582617, -4.346272141329937888, -32.91110030500001216 ) ) ;
#27526=CARTESIAN_POINT ( 'NONE',  ( 3.375516224911112584, -2.766870103071181308, -23.99674734060000603 ) ) ;
#27558=CARTESIAN_POINT ( 'NONE',  ( 0.5877407897813130555, -4.297347728519515186, -0.3731240480000022619 ) ) ;
#27559=CARTESIAN_POINT ( 'NONE',  ( -1.058439502263211374, 6.005994971325610443, -19.23583244400001036 ) ) ;
#27576=CARTESIAN_POINT ( 'NONE',  ( -6.277996069133942925, 1.777976852108807737, -7.310827254900003069 ) ) ;
#27600=CARTESIAN_POINT ( 'NONE',  ( -5.530047734074942767, 3.478668956039820959, -9.845475902800000512 ) ) ;
#27654=CARTESIAN_POINT ( 'NONE',  ( 2.561732861602287858, -4.873875974281082435, -34.20721934060000535 ) ) ;
#27670=CARTESIAN_POINT ( 'NONE',  ( -3.754118416966668814, 2.080634641777292071, -0.6999999999999992895 ) ) ;
#27671=CARTESIAN_POINT ( 'NONE',  ( 3.691964249065762260, -4.599677940684276933, -2.105321867100004685 ) ) ;
#27675=CARTESIAN_POINT ( 'NONE',  ( -1.657635364023947400, -6.345118362804027079, -13.15022317840000632 ) ) ;
#27676=CARTESIAN_POINT ( 'NONE',  ( 4.198532171030673332, 1.238783022246746413, -35.53159726780000227 ) ) ;
#27706=EDGE_CURVE ( 'NONE', #27907, #23432, #28799, .T. ) ;
#27712=CARTESIAN_POINT ( 'NONE',  ( -1.949381390262891589, -5.750991590113663676, -0.5756305127000010957 ) ) ;
#27713=CARTESIAN_POINT ( 'NONE',  ( -2.258375515291465963, 5.046176096958239654, -21.73780126170000671 ) ) ;
#27731=CARTESIAN_POINT ( 'NONE',  ( 0.5074138422395748638, -6.503547975687064664, -9.393384211799999051 ) ) ;
#27732=ORIENTED_EDGE ( 'NONE', *, *, #133, .F. ) ;
#27754=CARTESIAN_POINT ( 'NONE',  ( -3.950034095761355335, 2.484763540022569384, -10.44547590280000371 ) ) ;
#27791=( BOUNDED_SURFACE ( )  B_SPLINE_SURFACE ( 5, 5, ( 
 ( #29460, #27106, #22393, #3639, #8197, #1135 ),
 ( #3330, #3180, #15760, #30237, #8509, #13234 ),
 ( #24905, #837, #10727, #20641, #17947, #27558 ),
 ( #27712, #15451, #29765, #27879, #3485, #6003 ),
 ( #22850, #17798, #25053, #15602, #20175, #27409 ),
 ( #20327, #12937, #20483, #18268, #30084, #12784 ),
 ( #25205, #13081, #20021, #22547, #23009, #1298 ),
 ( #6324, #10581, #29926, #15919, #10892, #29618 ),
 ( #22692, #18110, #8050, #990, #17645, #10429 ),
 ( #5847, #8352, #27257, #6158, #25372, #3811 ),
 ( #13398, #5694, #1457, #11050, #8670, #15301 ),
 ( #28654, #28498, #30407, #25843, #21116, #30562 ),
 ( #28030, #8990, #13877, #25688, #13716, #16076 ),
 ( #25527, #6943, #4119, #7101, #13561, #1769 ),
 ( #23484, #11359, #23324, #1922, #2076, #9139 ),
 ( #23168, #20956, #18590, #18742, #16228, #28186 ),
 ( #30870, #11827, #11514, #6475, #4279, #30712 ),
 ( #2236, #3963, #6629, #18901, #28343, #6789 ),
 ( #1609, #11198, #20800, #8828, #4433, #18433 ),
 ( #16385, #25993, #14037, #23639, #11668, #21266 ),
 ( #31019, #26148, #9299, #21428, #16539, #23790 ),
 ( #4580, #14188, #9455, #19059, #345, #16687 ),
 ( #2537, #16849, #24405, #14809, #14502, #4746 ),
 ( #21731, #14655, #22194, #14959, #26757, #29422 ),
 ( #19374, #9771, #7560, #9927, #26298, #23953 ),
 ( #12432, #24099, #26917, #19840, #10086, #19528 ),
 ( #28964, #7406, #22050, #12125, #2837, #5193 ),
 ( #21898, #10238, #29116, #183, #19214, #17005 ),
 ( #500, #2388, #17151, #19680, #26607, #24558 ),
 ( #14352, #5047, #29265, #24243, #7259, #2685 ),
 ( #11973, #21585, #32, #7705, #9614, #28796 ),
 ( #12285, #26455, #4898, #17311, #5354, #2996 ),
 ( #12586, #651, #18070, #8316, #25013, #5815 ),
 ( #10691, #3446, #17911, #22655, #7856, #20141 ),
 ( #8013, #15560, #5965, #5660, #27066, #27519 ),
 ( #15413, #13362, #6121, #25169, #20601, #22509 ),
 ( #956, #29888, #1098, #17460, #15111, #13048 ),
 ( #15259, #27675, #11010, #1261, #20285, #17756 ),
 ( #29732, #13196, #24869, #3601, #22808, #3297 ),
 ( #10858, #5504, #24705, #20443, #30041, #3143 ),
 ( #15715, #8474, #12741, #22354, #25328, #10546 ),
 ( #3771, #801, #1417, #12901, #22970, #10391 ),
 ( #8160, #27376, #17611, #27219, #29577, #19982 ),
 ( #2041, #20759, #11786, #18226, #6438, #16037 ),
 ( #25653, #27993, #6594, #6749, #13841, #3927 ),
 ( #13521, #30364, #15886, #30198, #8629, #14151 ),
 ( #27834, #13680, #8793, #23451, #6286, #16500 ),
 ( #16191, #16348, #11326, #25489, #18396, #4083 ),
 ( #20923, #23284, #1727, #4393, #26111, #25807 ),
 ( #30525, #28154, #8953, #6898, #23134, #18552 ),
 ( #4239, #1881, #11480, #1576, #11162, #2197 ),
 ( #11630, #21081, #30829, #21228, #30678, #9105 ),
 ( #18705, #28304, #25957, #13999, #23605, #9256 ),
 ( #18865, #28462, #4549, #23756, #24208, #16964 ),
 ( #5010, #21392, #2502, #7218, #21544, #29079 ),
 ( #19177, #9414, #21859, #26421, #19336, #26879 ),
 ( #30983, #2807, #17271, #26718, #310, #7667 ),
 ( #19020, #28927, #5320, #14618, #2648, #7372 ),
 ( #12090, #16807, #14924, #21698, #12242, #14312 ),
 ( #4863, #147, #9888, #14464, #24064, #24521 ),
 ( #12299, #7523, #2958, #17118, #28621, #5155 ),
 ( #14767, #9728, #12399, #7061, #24366, #26262 ),
 ( #26570, #19491, #22010, #23917, #467, #10048 ),
 ( #16651, #19644, #29228, #4701, #2352, #11936 ),
 ( #9580, #28764, #3412, #29541, #10656, #13163 ),
 ( #29386, #27183, #22469, #19948, #919, #27031 ),
 ( #15222, #15074, #12702, #24672, #20109, #12552 ),
 ( #3106, #22159, #19800, #10357, #7976, #3260 ),
 ( #764, #10510, #13014, #29698, #5468, #22312 ),
 ( #22771, #8123, #17576, #5622, #24828, #17425 ),
 ( #17720, #12865, #27338, #5778, #15378, #15528 ),
 ( #27481, #7825, #616, #24976, #22625, #20247 ),
 ( #8282, #1066, #17877, #29848, #5928, #25133 ),
 ( #3569, #10201, #28718, #21957, #2757, #7471 ),
 ( #14568, #19747, #9993, #26666, #17067, #10150 ),
 ( #5108, #19592, #24308, #9527, #21798, #26516 ),
 ( #17216, #7621, #7324, #7166, #29173, #24158 ),
 ( #15026, #7774, #26822, #22259, #2599, #12186 ),
 ( #410, #12351, #19124, #16753, #14717, #5267 ),
 ( #29330, #12650, #2905, #14878, #19434, #253 ),
 ( #24470, #16909, #12497, #22108, #4957, #9838 ),
 ( #24620, #26370, #29025, #566, #17372, #26978 ),
 ( #4816, #14411, #5417, #3054, #24012, #2452 ),
 ( #12043, #21650, #98, #9677, #19280, #28871 ),
 ( #24535, #2820, #17288, #12566, #7992, #29556 ),
 ( #24384, #2516, #5483, #24685, #12411, #26434 ),
 ( #22172, #19506, #7836, #4874, #29400, #161 ),
 ( #22029, #322, #480, #28942, #9904, #14784 ),
 ( #14632, #16980, #29243, #14478, #17439, #26585 ),
 ( #24077, #2664, #12260, #10062, #21876, #24222 ),
 ( #2976, #19658, #9745, #19350, #7681, #19962 ),
 ( #17131, #5025, #29093, #632, #12717, #26894 ),
 ( #26732, #5333, #7539, #3120, #12102, #5170 ),
 ( #14937, #10214, #19817, #21711, #7384, #27046 ),
 ( #15091, #22329, #779, #10371, #22483, #18048 ),
 ( #22636, #24990, #11144, #23116, #18208, #15392 ),
 ( #20123, #15868, #1240, #932, #17590, #25308 ),
 ( #10837, #27199, #29863, #3425, #17735, #3750 ),
 ( #13027, #5638, #27654, #1079, #15541, #1556 ),
 ( #6096, #20741, #25471, #15694, #30341, #10670 ),
 ( #20265, #8451, #20423, #15235, #24845, #22787 ),
 ( #30016, #3581, #10990, #8295, #17890, #3274 ),
 ( #13344, #10525, #22950, #27496, #29711, #5942 ),
 ( #25146, #12879, #13176, #27352, #1394, #8139 ),
 ( #5794, #20582, #30178, #8608, #27815, #6266 ),
 ( #3905, #13499, #2332, #16170, #25935, #23896 ),
 ( #25634, #23431, #9085, #23736, #13659, #30504 ),
 ( #8773, #21520, #11916, #1858, #18379, #11458 ) ),
 .UNSPECIFIED., .F., .F., .T. ) 
 B_SPLINE_SURFACE_WITH_KNOTS ( ( 6, 3, 3, 3, 3, 3, 3, 3, 3, 3, 3, 3, 3, 3, 3, 3, 3, 3, 3, 3, 3, 3, 3, 3, 3, 3, 3, 3, 3, 3, 3, 3, 3, 3, 3, 6 ),
 ( 6, 6 ),
 ( 0.000000000000000000, 11.38862009670000042, 23.17260734259999921, 34.79167593860000096, 46.25425528950000142, 57.87229377410000097, 69.67120816000000616, 81.20502170430000888, 92.80704244429999505, 104.1208912059999960, 115.9269080290000034, 127.3307717769999954, 139.1306782750000082, 150.7654282180000109, 162.2434640489999822, 173.6637378899999931, 185.2020570420000070, 194.1769840820000184, 203.3038760180000111, 212.5853790139999830, 224.1393301889999918, 235.6932813650000185, 246.8715721779999797, 258.4996770380000157, 270.1277818960000445, 281.7035649139999691, 293.2822232819999613, 304.6732510989999696, 316.1434960830000023, 327.6894369340000139, 339.2353777880000507, 350.7813186390000055, 362.5843219139999860, 374.0573691039999744, 385.8560256170000002, 397.5961180479999939 ),
 ( 8.337129679329999377, 16.67425935869999876 ),
 .UNSPECIFIED. ) 
 GEOMETRIC_REPRESENTATION_ITEM ( )  RATIONAL_B_SPLINE_SURFACE ( (
 ( 0.2500000000000000000, 0.2500000000000000000, 0.2999999999999999889, 0.4000000000000000222, 0.5999999999999999778, 1.000000000000000000),
 ( 0.2500000000000000000, 0.2500000000000000000, 0.2999999999999999889, 0.4000000000000000222, 0.5999999999999999778, 1.000000000000000000),
 ( 0.2500000000000000000, 0.2500000000000000000, 0.2999999999999999889, 0.4000000000000000222, 0.5999999999999999778, 1.000000000000000000),
 ( 0.2500000000000000000, 0.2500000000000000000, 0.2999999999999999889, 0.4000000000000000222, 0.5999999999999999778, 1.000000000000000000),
 ( 0.2500000000000000000, 0.2500000000000000000, 0.2999999999999999889, 0.4000000000000000222, 0.5999999999999999778, 1.000000000000000000),
 ( 0.2500000000000000000, 0.2500000000000000000, 0.2999999999999999889, 0.4000000000000000222, 0.5999999999999999778, 1.000000000000000000),
 ( 0.2500000000000000000, 0.2500000000000000000, 0.2999999999999999889, 0.4000000000000000222, 0.5999999999999999778, 1.000000000000000000),
 ( 0.2500000000000000000, 0.2500000000000000000, 0.2999999999999999889, 0.4000000000000000222, 0.5999999999999999778, 1.000000000000000000),
 ( 0.2500000000000000000, 0.2500000000000000000, 0.2999999999999999889, 0.4000000000000000222, 0.5999999999999999778, 1.000000000000000000),
 ( 0.2500000000000000000, 0.2500000000000000000, 0.2999999999999999889, 0.4000000000000000222, 0.5999999999999999778, 1.000000000000000000),
 ( 0.2500000000000000000, 0.2500000000000000000, 0.2999999999999999889, 0.4000000000000000222, 0.5999999999999999778, 1.000000000000000000),
 ( 0.2500000000000000000, 0.2500000000000000000, 0.2999999999999999889, 0.4000000000000000222, 0.5999999999999999778, 1.000000000000000000),
 ( 0.2500000000000000000, 0.2500000000000000000, 0.2999999999999999889, 0.4000000000000000222, 0.5999999999999999778, 1.000000000000000000),
 ( 0.2500000000000000000, 0.2500000000000000000, 0.2999999999999999889, 0.4000000000000000222, 0.5999999999999999778, 1.000000000000000000),
 ( 0.2500000000000000000, 0.2500000000000000000, 0.2999999999999999889, 0.4000000000000000222, 0.5999999999999999778, 1.000000000000000000),
 ( 0.2500000000000000000, 0.2500000000000000000, 0.2999999999999999889, 0.4000000000000000222, 0.5999999999999999778, 1.000000000000000000),
 ( 0.2500000000000000000, 0.2500000000000000000, 0.2999999999999999889, 0.4000000000000000222, 0.5999999999999999778, 1.000000000000000000),
 ( 0.2500000000000000000, 0.2500000000000000000, 0.2999999999999999889, 0.4000000000000000222, 0.5999999999999999778, 1.000000000000000000),
 ( 0.2500000000000000000, 0.2500000000000000000, 0.2999999999999999889, 0.4000000000000000222, 0.5999999999999999778, 1.000000000000000000),
 ( 0.2500000000000000000, 0.2500000000000000000, 0.2999999999999999889, 0.4000000000000000222, 0.5999999999999999778, 1.000000000000000000),
 ( 0.2500000000000000000, 0.2500000000000000000, 0.2999999999999999889, 0.4000000000000000222, 0.5999999999999999778, 1.000000000000000000),
 ( 0.2500000000000000000, 0.2500000000000000000, 0.2999999999999999889, 0.4000000000000000222, 0.5999999999999999778, 1.000000000000000000),
 ( 0.2500000000000000000, 0.2500000000000000000, 0.2999999999999999889, 0.4000000000000000222, 0.5999999999999999778, 1.000000000000000000),
 ( 0.2500000000000000000, 0.2500000000000000000, 0.2999999999999999889, 0.4000000000000000222, 0.5999999999999999778, 1.000000000000000000),
 ( 0.2500000000000000000, 0.2500000000000000000, 0.2999999999999999889, 0.4000000000000000222, 0.5999999999999999778, 1.000000000000000000),
 ( 0.2500000000000000000, 0.2500000000000000000, 0.2999999999999999889, 0.4000000000000000222, 0.5999999999999999778, 1.000000000000000000),
 ( 0.2500000000000000000, 0.2500000000000000000, 0.2999999999999999889, 0.4000000000000000222, 0.5999999999999999778, 1.000000000000000000),
 ( 0.2500000000000000000, 0.2500000000000000000, 0.2999999999999999889, 0.4000000000000000222, 0.5999999999999999778, 1.000000000000000000),
 ( 0.2500000000000000000, 0.2500000000000000000, 0.2999999999999999889, 0.4000000000000000222, 0.5999999999999999778, 1.000000000000000000),
 ( 0.2500000000000000000, 0.2500000000000000000, 0.2999999999999999889, 0.4000000000000000222, 0.5999999999999999778, 1.000000000000000000),
 ( 0.2500000000000000000, 0.2500000000000000000, 0.2999999999999999889, 0.4000000000000000222, 0.5999999999999999778, 1.000000000000000000),
 ( 0.2500000000000000000, 0.2500000000000000000, 0.2999999999999999889, 0.4000000000000000222, 0.5999999999999999778, 1.000000000000000000),
 ( 0.2500000000000000000, 0.2500000000000000000, 0.2999999999999999889, 0.4000000000000000222, 0.5999999999999999778, 1.000000000000000000),
 ( 0.2500000000000000000, 0.2500000000000000000, 0.2999999999999999889, 0.4000000000000000222, 0.5999999999999999778, 1.000000000000000000),
 ( 0.2500000000000000000, 0.2500000000000000000, 0.2999999999999999889, 0.4000000000000000222, 0.5999999999999999778, 1.000000000000000000),
 ( 0.2500000000000000000, 0.2500000000000000000, 0.2999999999999999889, 0.4000000000000000222, 0.5999999999999999778, 1.000000000000000000),
 ( 0.2500000000000000000, 0.2500000000000000000, 0.2999999999999999889, 0.4000000000000000222, 0.5999999999999999778, 1.000000000000000000),
 ( 0.2500000000000000000, 0.2500000000000000000, 0.2999999999999999889, 0.4000000000000000222, 0.5999999999999999778, 1.000000000000000000),
 ( 0.2500000000000000000, 0.2500000000000000000, 0.2999999999999999889, 0.4000000000000000222, 0.5999999999999999778, 1.000000000000000000),
 ( 0.2500000000000000000, 0.2500000000000000000, 0.2999999999999999889, 0.4000000000000000222, 0.5999999999999999778, 1.000000000000000000),
 ( 0.2500000000000000000, 0.2500000000000000000, 0.2999999999999999889, 0.4000000000000000222, 0.5999999999999999778, 1.000000000000000000),
 ( 0.2500000000000000000, 0.2500000000000000000, 0.2999999999999999889, 0.4000000000000000222, 0.5999999999999999778, 1.000000000000000000),
 ( 0.2500000000000000000, 0.2500000000000000000, 0.2999999999999999889, 0.4000000000000000222, 0.5999999999999999778, 1.000000000000000000),
 ( 0.2500000000000000000, 0.2500000000000000000, 0.2999999999999999889, 0.4000000000000000222, 0.5999999999999999778, 1.000000000000000000),
 ( 0.2500000000000000000, 0.2500000000000000000, 0.2999999999999999889, 0.4000000000000000222, 0.5999999999999999778, 1.000000000000000000),
 ( 0.2500000000000000000, 0.2500000000000000000, 0.2999999999999999889, 0.4000000000000000222, 0.5999999999999999778, 1.000000000000000000),
 ( 0.2500000000000000000, 0.2500000000000000000, 0.2999999999999999889, 0.4000000000000000222, 0.5999999999999999778, 1.000000000000000000),
 ( 0.2500000000000000000, 0.2500000000000000000, 0.2999999999999999889, 0.4000000000000000222, 0.5999999999999999778, 1.000000000000000000),
 ( 0.2500000000000000000, 0.2500000000000000000, 0.2999999999999999889, 0.4000000000000000222, 0.5999999999999999778, 1.000000000000000000),
 ( 0.2500000000000000000, 0.2500000000000000000, 0.2999999999999999889, 0.4000000000000000222, 0.5999999999999999778, 1.000000000000000000),
 ( 0.2500000000000000000, 0.2500000000000000000, 0.2999999999999999889, 0.4000000000000000222, 0.5999999999999999778, 1.000000000000000000),
 ( 0.2500000000000000000, 0.2500000000000000000, 0.2999999999999999889, 0.4000000000000000222, 0.5999999999999999778, 1.000000000000000000),
 ( 0.2500000000000000000, 0.2500000000000000000, 0.2999999999999999889, 0.4000000000000000222, 0.5999999999999999778, 1.000000000000000000),
 ( 0.2500000000000000000, 0.2500000000000000000, 0.2999999999999999889, 0.4000000000000000222, 0.5999999999999999778, 1.000000000000000000),
 ( 0.2500000000000000000, 0.2500000000000000000, 0.2999999999999999889, 0.4000000000000000222, 0.5999999999999999778, 1.000000000000000000),
 ( 0.2500000000000000000, 0.2500000000000000000, 0.2999999999999999889, 0.4000000000000000222, 0.5999999999999999778, 1.000000000000000000),
 ( 0.2500000000000000000, 0.2500000000000000000, 0.2999999999999999889, 0.4000000000000000222, 0.5999999999999999778, 1.000000000000000000),
 ( 0.2500000000000000000, 0.2500000000000000000, 0.2999999999999999889, 0.4000000000000000222, 0.5999999999999999778, 1.000000000000000000),
 ( 0.2500000000000000000, 0.2500000000000000000, 0.2999999999999999889, 0.4000000000000000222, 0.5999999999999999778, 1.000000000000000000),
 ( 0.2500000000000000000, 0.2500000000000000000, 0.2999999999999999889, 0.4000000000000000222, 0.5999999999999999778, 1.000000000000000000),
 ( 0.2500000000000000000, 0.2500000000000000000, 0.2999999999999999889, 0.4000000000000000222, 0.5999999999999999778, 1.000000000000000000),
 ( 0.2500000000000000000, 0.2500000000000000000, 0.2999999999999999889, 0.4000000000000000222, 0.5999999999999999778, 1.000000000000000000),
 ( 0.2500000000000000000, 0.2500000000000000000, 0.2999999999999999889, 0.4000000000000000222, 0.5999999999999999778, 1.000000000000000000),
 ( 0.2500000000000000000, 0.2500000000000000000, 0.2999999999999999889, 0.4000000000000000222, 0.5999999999999999778, 1.000000000000000000),
 ( 0.2500000000000000000, 0.2500000000000000000, 0.2999999999999999889, 0.4000000000000000222, 0.5999999999999999778, 1.000000000000000000),
 ( 0.2500000000000000000, 0.2500000000000000000, 0.2999999999999999889, 0.4000000000000000222, 0.5999999999999999778, 1.000000000000000000),
 ( 0.2500000000000000000, 0.2500000000000000000, 0.2999999999999999889, 0.4000000000000000222, 0.5999999999999999778, 1.000000000000000000),
 ( 0.2500000000000000000, 0.2500000000000000000, 0.2999999999999999889, 0.4000000000000000222, 0.5999999999999999778, 1.000000000000000000),
 ( 0.2500000000000000000, 0.2500000000000000000, 0.2999999999999999889, 0.4000000000000000222, 0.5999999999999999778, 1.000000000000000000),
 ( 0.2500000000000000000, 0.2500000000000000000, 0.2999999999999999889, 0.4000000000000000222, 0.5999999999999999778, 1.000000000000000000),
 ( 0.2500000000000000000, 0.2500000000000000000, 0.2999999999999999889, 0.4000000000000000222, 0.5999999999999999778, 1.000000000000000000),
 ( 0.2500000000000000000, 0.2500000000000000000, 0.2999999999999999889, 0.4000000000000000222, 0.5999999999999999778, 1.000000000000000000),
 ( 0.2500000000000000000, 0.2500000000000000000, 0.2999999999999999889, 0.4000000000000000222, 0.5999999999999999778, 1.000000000000000000),
 ( 0.2500000000000000000, 0.2500000000000000000, 0.2999999999999999889, 0.4000000000000000222, 0.5999999999999999778, 1.000000000000000000),
 ( 0.2500000000000000000, 0.2500000000000000000, 0.2999999999999999889, 0.4000000000000000222, 0.5999999999999999778, 1.000000000000000000),
 ( 0.2500000000000000000, 0.2500000000000000000, 0.2999999999999999889, 0.4000000000000000222, 0.5999999999999999778, 1.000000000000000000),
 ( 0.2500000000000000000, 0.2500000000000000000, 0.2999999999999999889, 0.4000000000000000222, 0.5999999999999999778, 1.000000000000000000),
 ( 0.2500000000000000000, 0.2500000000000000000, 0.2999999999999999889, 0.4000000000000000222, 0.5999999999999999778, 1.000000000000000000),
 ( 0.2500000000000000000, 0.2500000000000000000, 0.2999999999999999889, 0.4000000000000000222, 0.5999999999999999778, 1.000000000000000000),
 ( 0.2500000000000000000, 0.2500000000000000000, 0.2999999999999999889, 0.4000000000000000222, 0.5999999999999999778, 1.000000000000000000),
 ( 0.2500000000000000000, 0.2500000000000000000, 0.2999999999999999889, 0.4000000000000000222, 0.5999999999999999778, 1.000000000000000000),
 ( 0.2500000000000000000, 0.2500000000000000000, 0.2999999999999999889, 0.4000000000000000222, 0.5999999999999999778, 1.000000000000000000),
 ( 0.2500000000000000000, 0.2500000000000000000, 0.2999999999999999889, 0.4000000000000000222, 0.5999999999999999778, 1.000000000000000000),
 ( 0.2500000000000000000, 0.2500000000000000000, 0.2999999999999999889, 0.4000000000000000222, 0.5999999999999999778, 1.000000000000000000),
 ( 0.2500000000000000000, 0.2500000000000000000, 0.2999999999999999889, 0.4000000000000000222, 0.5999999999999999778, 1.000000000000000000),
 ( 0.2500000000000000000, 0.2500000000000000000, 0.2999999999999999889, 0.4000000000000000222, 0.5999999999999999778, 1.000000000000000000),
 ( 0.2500000000000000000, 0.2500000000000000000, 0.2999999999999999889, 0.4000000000000000222, 0.5999999999999999778, 1.000000000000000000),
 ( 0.2500000000000000000, 0.2500000000000000000, 0.2999999999999999889, 0.4000000000000000222, 0.5999999999999999778, 1.000000000000000000),
 ( 0.2500000000000000000, 0.2500000000000000000, 0.2999999999999999889, 0.4000000000000000222, 0.5999999999999999778, 1.000000000000000000),
 ( 0.2500000000000000000, 0.2500000000000000000, 0.2999999999999999889, 0.4000000000000000222, 0.5999999999999999778, 1.000000000000000000),
 ( 0.2500000000000000000, 0.2500000000000000000, 0.2999999999999999889, 0.4000000000000000222, 0.5999999999999999778, 1.000000000000000000),
 ( 0.2500000000000000000, 0.2500000000000000000, 0.2999999999999999889, 0.4000000000000000222, 0.5999999999999999778, 1.000000000000000000),
 ( 0.2500000000000000000, 0.2500000000000000000, 0.2999999999999999889, 0.4000000000000000222, 0.5999999999999999778, 1.000000000000000000),
 ( 0.2500000000000000000, 0.2500000000000000000, 0.2999999999999999889, 0.4000000000000000222, 0.5999999999999999778, 1.000000000000000000),
 ( 0.2500000000000000000, 0.2500000000000000000, 0.2999999999999999889, 0.4000000000000000222, 0.5999999999999999778, 1.000000000000000000),
 ( 0.2500000000000000000, 0.2500000000000000000, 0.2999999999999999889, 0.4000000000000000222, 0.5999999999999999778, 1.000000000000000000),
 ( 0.2500000000000000000, 0.2500000000000000000, 0.2999999999999999889, 0.4000000000000000222, 0.5999999999999999778, 1.000000000000000000),
 ( 0.2500000000000000000, 0.2500000000000000000, 0.2999999999999999889, 0.4000000000000000222, 0.5999999999999999778, 1.000000000000000000),
 ( 0.2500000000000000000, 0.2500000000000000000, 0.2999999999999999889, 0.4000000000000000222, 0.5999999999999999778, 1.000000000000000000),
 ( 0.2500000000000000000, 0.2500000000000000000, 0.2999999999999999889, 0.4000000000000000222, 0.5999999999999999778, 1.000000000000000000),
 ( 0.2500000000000000000, 0.2500000000000000000, 0.2999999999999999889, 0.4000000000000000222, 0.5999999999999999778, 1.000000000000000000),
 ( 0.2500000000000000000, 0.2500000000000000000, 0.2999999999999999889, 0.4000000000000000222, 0.5999999999999999778, 1.000000000000000000),
 ( 0.2500000000000000000, 0.2500000000000000000, 0.2999999999999999889, 0.4000000000000000222, 0.5999999999999999778, 1.000000000000000000),
 ( 0.2500000000000000000, 0.2500000000000000000, 0.2999999999999999889, 0.4000000000000000222, 0.5999999999999999778, 1.000000000000000000),
 ( 0.2500000000000000000, 0.2500000000000000000, 0.2999999999999999889, 0.4000000000000000222, 0.5999999999999999778, 1.000000000000000000),
 ( 0.2500000000000000000, 0.2500000000000000000, 0.2999999999999999889, 0.4000000000000000222, 0.5999999999999999778, 1.000000000000000000),
 ( 0.2500000000000000000, 0.2500000000000000000, 0.2999999999999999889, 0.4000000000000000222, 0.5999999999999999778, 1.000000000000000000),
 ( 0.2500000000000000000, 0.2500000000000000000, 0.2999999999999999889, 0.4000000000000000222, 0.5999999999999999778, 1.000000000000000000) ) ) 
 REPRESENTATION_ITEM ( '' )  SURFACE ( )  );
#27807=PLANE ( 'NONE',  #26834 ) ;
#27815=CARTESIAN_POINT ( 'NONE',  ( 3.155489075140835542, 3.034105443485036968, -35.82341724620001600 ) ) ;
#27831=CARTESIAN_POINT ( 'NONE',  ( -3.324062773583611907, -4.387625903868788591, -2.728945369300002977 ) ) ;
#27834=CARTESIAN_POINT ( 'NONE',  ( -3.283272085064022239, -5.616145207998583189, -15.68182079290000175 ) ) ;
#27835=CARTESIAN_POINT ( 'NONE',  ( 5.672553144689285176, -0.9485505809898806540, -35.74517599850000948 ) ) ;
#27847=FACE_OUTER_BOUND ( 'NONE', #11534, .T. ) ;
#27870=CARTESIAN_POINT ( 'NONE',  ( 2.653975030832389059, 2.820913939037494433, -35.69999999999999574 ) ) ;
#27879=CARTESIAN_POINT ( 'NONE',  ( -1.531656806707240248, -4.518636249346831946, -1.513130512700005426 ) ) ;
#27880=CARTESIAN_POINT ( 'NONE',  ( -4.217400109093552452, 2.917745507991547971, -24.53029765530000006 ) ) ;
#27896=CARTESIAN_POINT ( 'NONE',  ( 1.403799475828179766, 5.569137675590418723, -17.05080441500000177 ) ) ;
#27907=VERTEX_POINT ( 'NONE', #15343 ) ;
#27921=CARTESIAN_POINT ( 'NONE',  ( -3.941349475653407985, -1.876729865818548282, -12.47655742010000068 ) ) ;
#27989=CARTESIAN_POINT ( 'NONE',  ( -4.757675747652303500, -1.918655839533711660, -0.05969743450000113139 ) ) ;
#27993=CARTESIAN_POINT ( 'NONE',  ( 4.315341029122434335, -4.279276102762477940, -15.66112212870000242 ) ) ;
#27994=CARTESIAN_POINT ( 'NONE',  ( -0.3609073012553025150, 5.149274899367955349, -33.95768930509999706 ) ) ;
#28030=CARTESIAN_POINT ( 'NONE',  ( -3.673964118181757943, -4.849481262180703744, -3.728945369300004753 ) ) ;
#28031=CARTESIAN_POINT ( 'NONE',  ( 0.2925910193319765096, 5.520737601085913937, -21.94418644580000688 ) ) ;
#28049=CARTESIAN_POINT ( 'NONE',  ( 6.118976883090258667, 2.212479739890888197, -26.51249766020000109 ) ) ;
#28071=CARTESIAN_POINT ( 'NONE',  ( 5.466312515054250198, -2.792605348973308477, -11.31474735219999772 ) ) ;
#28149=CARTESIAN_POINT ( 'NONE',  ( -4.646804529178800713, -0.2974863596997128767, -3.648838774900006854 ) ) ;
#28154=CARTESIAN_POINT ( 'NONE',  ( -3.057389860650357338, 5.459897439232808125, -17.27761783620000102 ) ) ;
#28175=CARTESIAN_POINT ( 'NONE',  ( 3.162069896769252431, -2.100311282821142100, -35.69999999999999574 ) ) ;
#28180=CARTESIAN_POINT ( 'NONE',  ( 3.363928025720356985, 1.758349587396049296, -35.70000000000000284 ) ) ;
#28186=CARTESIAN_POINT ( 'NONE',  ( -1.295942751353772238, 4.166547562507297187, -4.774955258300003891 ) ) ;
#28187=CARTESIAN_POINT ( 'NONE',  ( 0.1047326596782457986, -5.131546142535936994, -23.48138333260000010 ) ) ;
#28204=FACE_OUTER_BOUND ( 'NONE', #14907, .T. ) ;
#28210=ORIENTED_EDGE ( 'NONE', *, *, #133, .T. ) ;
#28224=CARTESIAN_POINT ( 'NONE',  ( -3.941349475653395551, -1.876729865818549392, -12.97655742010000246 ) ) ;
#28299=CARTESIAN_POINT ( 'NONE',  ( 2.521631941452528558, 3.946033397249446573, -4.700967428500005596 ) ) ;
#28304=CARTESIAN_POINT ( 'NONE',  ( 5.782996427689181651, 1.709881257618839356, -18.14190840230000390 ) ) ;
#28305=CARTESIAN_POINT ( 'NONE',  ( 4.051823674760409943, -0.6775361292690254000, -35.74517599850000948 ) ) ;
#28322=CARTESIAN_POINT ( 'NONE',  ( -1.354272418126746702, -5.070319514866119981, -0.7001538049033677602 ) ) ;
#28343=CARTESIAN_POINT ( 'NONE',  ( 4.347198243976411192, 0.5700341643805815206, -6.126979598399997506 ) ) ;
#28344=CARTESIAN_POINT ( 'NONE',  ( -5.367600138795724618, 3.713494282866228069, -24.86779765530000574 ) ) ;
#28360=CARTESIAN_POINT ( 'NONE',  ( -0.6320852424383932577, 6.069672320066970883, -25.88903409330001182 ) ) ;
#28388=CARTESIAN_POINT ( 'NONE',  ( 6.482330152203070739, 0.4632910120546396282, -14.04454535870000598 ) ) ;
#28458=CARTESIAN_POINT ( 'NONE',  ( 0.1708583496781435063, 4.358252033550405358, -7.937690181100000686 ) ) ;
#28462=CARTESIAN_POINT ( 'NONE',  ( 5.320018516182488000, -2.211191048809329374, -18.47122516809999837 ) ) ;
#28492=CARTESIAN_POINT ( 'NONE',  ( 0.7056244670274119946, 4.148270963307473913, -35.69999999999998153 ) ) ;
#28498=CARTESIAN_POINT ( 'NONE',  ( -1.102325287918849650, -5.983340188646091740, -4.125234013000008915 ) ) ;
#28499=CARTESIAN_POINT ( 'NONE',  ( 0.6138679561251692007, 4.311712124478116692, -28.50600711720001001 ) ) ;
#28505=CARTESIAN_POINT ( 'NONE',  ( -3.630162863991669209, -2.403661707492378508, -6.889929326000000742 ) ) ;
#28516=CARTESIAN_POINT ( 'NONE',  ( 3.499930668447871707, 4.992711500626898058, -29.21106724380000230 ) ) ;
#28539=CARTESIAN_POINT ( 'NONE',  ( 1.942707423728255778, -5.758494596869851989, -15.26414732020000464 ) ) ;
#28617=CARTESIAN_POINT ( 'NONE',  ( 2.773795135624238295, 4.340636736956414943, -4.263467428500004708 ) ) ;
#28621=CARTESIAN_POINT ( 'NONE',  ( -0.7560282158644051620, 4.289996408053716515, -20.33583244400001178 ) ) ;
#28649=CARTESIAN_POINT ( 'NONE',  ( 0.2553064023551063766, 4.393912938272285906, -35.69999999999999574 ) ) ;
#28651=CARTESIAN_POINT ( 'NONE',  ( -3.797496571118017528, -0.6966955563414738428, -0.6999999999999995115 ) ) ;
#28654=CARTESIAN_POINT ( 'NONE',  ( -1.102325287918849650, -5.983340188646091740, -3.525234013000005717 ) ) ;
#28655=CARTESIAN_POINT ( 'NONE',  ( 5.536217179945332134, 2.001767383715431503, -25.51249766019999399 ) ) ;
#28662=CARTESIAN_POINT ( 'NONE',  ( -4.646804529178781173, -0.2974863596997279203, -4.148838774900000637 ) ) ;
#28671=CARTESIAN_POINT ( 'NONE',  ( -4.273414424137721213, 4.913340199448848367, -28.58728588869999143 ) ) ;
#28694=CARTESIAN_POINT ( 'NONE',  ( 5.320018516182488000, -2.211191048809329374, -17.27122516810000619 ) ) ;
#28718=CARTESIAN_POINT ( 'NONE',  ( 0.1206012444329082195, -5.909053133798479962, -25.41888333260000721 ) ) ;
#28759=CARTESIAN_POINT ( 'NONE',  ( 4.347198243976404974, 0.5700341643805826308, -5.626979598400000171 ) ) ;
#28764=CARTESIAN_POINT ( 'NONE',  ( 1.771049722044198971, -6.234229536879996481, -21.89535708919999735 ) ) ;
#28791=CARTESIAN_POINT ( 'NONE',  ( 0.2353820488414976597, 4.569370376363825592, -35.70000000000000284 ) ) ;
#28796=CARTESIAN_POINT ( 'NONE',  ( -4.184186767956295405, -1.312611723764782523, -10.02323088899999881 ) ) ;
#28797=CARTESIAN_POINT ( 'NONE',  ( 4.370697773661015972, 1.580342671372847230, -26.01249766020000820 ) ) ;
#28799=( BOUNDED_CURVE ( )  B_SPLINE_CURVE ( 5, ( #16765, #26386, #14424, #24023, #13799, #2465 ),
 .UNSPECIFIED., .F., .T. ) 
 B_SPLINE_CURVE_WITH_KNOTS ( ( 6, 6 ),
 ( 1.352733214049999910, 7.601046855679999936 ),
 .UNSPECIFIED. ) 
 CURVE ( )  GEOMETRIC_REPRESENTATION_ITEM ( )  RATIONAL_B_SPLINE_CURVE ( ( 0.7240463347079999501, 0.5103476925150000065, 0.3838633578460000084, 0.3093277433949999655, 0.2672497422500000330, 0.2539127278980000124 ) ) 
 REPRESENTATION_ITEM ( '' )  );
#28803=CARTESIAN_POINT ( 'NONE',  ( 4.116710911288352648, -1.508563155650267884, -5.836105321700007842 ) ) ;
#28805=COLOUR_RGB ( '', 0.09019608, 0.27058824, 0.51372549) ;
#28835=CARTESIAN_POINT ( 'NONE',  ( 3.532196160932838502, -3.333259304328497485, -0.6997801443041695713 ) ) ;
#28839=CARTESIAN_POINT ( 'NONE',  ( -2.766209873889304394, 4.939907206908331183, -15.67761783620001204 ) ) ;
#28871=CARTESIAN_POINT ( 'NONE',  ( -3.878879136156893281, -1.961445906012333706, -27.96472909260000606 ) ) ;
#28923=CARTESIAN_POINT ( 'NONE',  ( -4.273751495587445604, 4.364932658710685587, -3.968732180600002657 ) ) ;
#28927=CARTESIAN_POINT ( 'NONE',  ( -4.663991843195165465, -3.413757688390889555, -19.47254627020000939 ) ) ;
#28942=CARTESIAN_POINT ( 'NONE',  ( 2.749945525234485988, 3.922844750473964748, -30.14856724380000230 ) ) ;
#28957=CARTESIAN_POINT ( 'NONE',  ( 0.6023992814822636266, 4.702695962538667729, -35.70000000000000284 ) ) ;
#28964=CARTESIAN_POINT ( 'NONE',  ( 5.967946066639521874, -1.056419632483374116, -8.771482634700005221 ) ) ;
#28965=CARTESIAN_POINT ( 'NONE',  ( 3.499930668453409055, 4.992711500635231836, -29.21106724380000230 ) ) ;
#28971=CARTESIAN_POINT ( 'NONE',  ( -3.941349475653395551, -1.876729865818549392, -12.97655742010000246 ) ) ;
#29000=CARTESIAN_POINT ( 'NONE',  ( 3.256742448429973624, 4.730705660258329281, -16.61259163650000303 ) ) ;
#29012=CARTESIAN_POINT ( 'NONE',  ( -2.825020644939634007, -4.425443225455641283, -0.6999999999999992895 ) ) ;
#29025=CARTESIAN_POINT ( 'NONE',  ( 3.104103280670445830, -4.533555713950848443, -28.13292313650000409 ) ) ;
#29072=CARTESIAN_POINT ( 'NONE',  ( 1.348918213770420316, 4.124136235849971577, -10.57047964830000275 ) ) ;
#29079=CARTESIAN_POINT ( 'NONE',  ( 2.992916622598568388, -2.824380467281232487, -18.03565260999999964 ) ) ;
#29093=CARTESIAN_POINT ( 'NONE',  ( -2.923929784071483073, -5.123485640109426420, -31.67642233980000555 ) ) ;
#29107=CARTESIAN_POINT ( 'NONE',  ( 1.325687545906950593, 4.708841374623678355, -35.69999999999998153 ) ) ;
#29116=CARTESIAN_POINT ( 'NONE',  ( 4.416054526660082580, -3.250752328011468961, -9.972776792900004850 ) ) ;
#29117=CARTESIAN_POINT ( 'NONE',  ( -3.866422574246632937, 4.445403037619903408, -27.58728588870000209 ) ) ;
#29122=CARTESIAN_POINT ( 'NONE',  ( -2.929853409778804263, 3.622264489389750874, -13.60352819869999763 ) ) ;
#29151=CARTESIAN_POINT ( 'NONE',  ( 1.270104287659547859, 5.038743611242932907, -16.05080441500000532 ) ) ;
#29173=CARTESIAN_POINT ( 'NONE',  ( -3.834000099192958810, 2.652495916366497841, -25.96779765529999651 ) ) ;
#29203=DIRECTION ( 'NONE',  ( 1.000000000000000000, 0.000000000000000000, 0.000000000000000000 ) ) ;
#29221=CARTESIAN_POINT ( 'NONE',  ( 4.416054526660082580, -3.250752328011468961, -7.972776792900008402 ) ) ;
#29228=CARTESIAN_POINT ( 'NONE',  ( 4.979326355943800131, -2.377326608238005790, -21.88180150030000348 ) ) ;
#29243=CARTESIAN_POINT ( 'NONE',  ( 5.869757812515316253, 0.5877190740209992104, -30.63116556699999649 ) ) ;
#29265=CARTESIAN_POINT ( 'NONE',  ( -3.925562765917044228, -3.929887376319241898, -10.81399163100000216 ) ) ;
#29266=CARTESIAN_POINT ( 'NONE',  ( -2.126050624815288614, 4.685496013473724020, -30.78885571289999845 ) ) ;
#29272=CARTESIAN_POINT ( 'NONE',  ( -4.274658871253798509, -0.8336587121505270037, -31.09652066320001040 ) ) ;
#29302=CARTESIAN_POINT ( 'NONE',  ( -4.180754675048095947, 1.217138862148074763, -16.30443125759999745 ) ) ;
#29330=CARTESIAN_POINT ( 'NONE',  ( 6.118976883090258667, 2.212479739890888197, -26.51249766020000109 ) ) ;
#29351=CARTESIAN_POINT ( 'NONE',  ( 2.458800944228217933, -3.193228378228379238, -0.6999999999999992895 ) ) ;
#29375=ADVANCED_FACE ( 'NONE', ( #27847 ), #16356, .T. ) ;
#29378=CARTESIAN_POINT ( 'NONE',  ( -4.184186767956290964, -1.312611723764788296, -9.523230888999998811 ) ) ;
#29386=CARTESIAN_POINT ( 'NONE',  ( -3.251750336246070461, -5.089746299513510763, -21.70891267860000795 ) ) ;
#29400=CARTESIAN_POINT ( 'NONE',  ( 0.6138679561251692007, 4.311712124478116692, -29.50600711719999936 ) ) ;
#29417=CARTESIAN_POINT ( 'NONE',  ( -4.301560380444131582, 2.091195337698785295, -0.6999999999999991784 ) ) ;
#29418=CARTESIAN_POINT ( 'NONE',  ( 2.223383862040879677, -3.430296892840221101, 0.3340606116999991215 ) ) ;
#29422=CARTESIAN_POINT ( 'NONE',  ( -1.831588579526997940, 3.958388136463042439, -7.731725184300007214 ) ) ;
#29423=CARTESIAN_POINT ( 'NONE',  ( 2.224662748255027633, -4.232576503996232198, -32.26971934059999825 ) ) ;
#29430=CARTESIAN_POINT ( 'NONE',  ( -3.500772897184936561, -3.093025330206538470, -33.83447003410000775 ) ) ;
#29460=CARTESIAN_POINT ( 'NONE',  ( 4.373195337096347224, -2.904765488536225515, 0.04124526979999709742 ) ) ;
#29461=CARTESIAN_POINT ( 'NONE',  ( -2.322678811625143780, -3.635533071076384015, -21.70891267860000795 ) ) ;
#29507=CARTESIAN_POINT ( 'NONE',  ( 0.4034208554058360541, -3.803105581716118344, -0.6999999999999992895 ) ) ;
#29541=CARTESIAN_POINT ( 'NONE',  ( 1.391539067366913018, -4.898323207587138128, -22.23285708920000658 ) ) ;
#29556=CARTESIAN_POINT ( 'NONE',  ( -4.346598770676703083, -0.007247149673123010061, -28.16856466009999593 ) ) ;
#29566=ORIENTED_EDGE ( 'NONE', *, *, #6199, .F. ) ;
#29573=CARTESIAN_POINT ( 'NONE',  ( -3.810063518243186120, 1.754619919559086139, -0.6999999999999995115 ) ) ;
#29574=CARTESIAN_POINT ( 'NONE',  ( 3.123710955063065509, -2.074832491810036039, 0.5412452697999986517 ) ) ;
#29577=CARTESIAN_POINT ( 'NONE',  ( 2.618538529469167653, 3.470429992801025154, -14.72796858840001022 ) ) ;
#29578=CARTESIAN_POINT ( 'NONE',  ( 3.503437880484523426, 2.636891074944038404, -31.86032172560000575 ) ) ;
#29586=CARTESIAN_POINT ( 'NONE',  ( 3.746497173757565413, -0.1670055334890632737, -35.69999999999999574 ) ) ;
#29606=VERTEX_POINT ( 'NONE', #19653 ) ;
#29618=CARTESIAN_POINT ( 'NONE',  ( 1.213582369797461258, 4.521795443253901148, -2.053410702900000828 ) ) ;
#29619=CARTESIAN_POINT ( 'NONE',  ( 4.354753084053725409, 0.1085053810021691101, -20.67661200060000226 ) ) ;
#29635=CARTESIAN_POINT ( 'NONE',  ( -4.101794773665658589, 5.071170285168458136, -13.60352819870000474 ) ) ;
#29665=CARTESIAN_POINT ( 'NONE',  ( 3.215880358400865280, -2.702085720338708974, -0.6999999999999992895 ) ) ;
#29677=SURFACE_SIDE_STYLE ('',( #25269 ) ) ;
#29698=CARTESIAN_POINT ( 'NONE',  ( -1.961220842236323536, 4.382205557898919857, -23.67530126170000315 ) ) ;
#29711=CARTESIAN_POINT ( 'NONE',  ( -3.554763430470067043, 2.566410659217312151, -34.96696136359999940 ) ) ;
#29727=CARTESIAN_POINT ( 'NONE',  ( -4.035443471795205461, 2.350095507017441410, -0.6999999999999992895 ) ) ;
#29732=CARTESIAN_POINT ( 'NONE',  ( -5.517889265940039145, -2.627421812126006451, -12.97655742010000246 ) ) ;
#29733=CARTESIAN_POINT ( 'NONE',  ( -2.705882613314523955, 5.963358562559473164, -31.12635571289999703 ) ) ;
#29765=CARTESIAN_POINT ( 'NONE',  ( -1.763726019828893321, -5.203278105301040846, -1.575630512700004537 ) ) ;
#29766=CARTESIAN_POINT ( 'NONE',  ( -2.322678811625146444, -3.635533071076381795, -21.20891267860001150 ) ) ;
#29781=CARTESIAN_POINT ( 'NONE',  ( 3.530284718056032833, 5.524446756132658898, -5.200967428500000267 ) ) ;
#29811=CARTESIAN_POINT ( 'NONE',  ( 3.514399168375105909, -2.498675756239369328, -0.6999999999999992895 ) ) ;
#29848=CARTESIAN_POINT ( 'NONE',  ( 3.713067847428462631, -3.043557113396612390, -24.93424734059999537 ) ) ;
#29863=CARTESIAN_POINT ( 'NONE',  ( 5.771960588451495511, -1.304678385556235165, -33.78377053309999667 ) ) ;
#29881=CARTESIAN_POINT ( 'NONE',  ( -3.854342479829299339, 1.502750475587120160, -0.6999999999999992895 ) ) ;
#29882=CARTESIAN_POINT ( 'NONE',  ( -1.531656806707240248, -4.518636249346831946, 0.3618694872999962397 ) ) ;
#29888=CARTESIAN_POINT ( 'NONE',  ( 3.550610403408205329, -5.007233058897099021, -12.72388893670000520 ) ) ;
#29889=CARTESIAN_POINT ( 'NONE',  ( 2.831388952324535691, -5.386915550550475551, -32.60721934059999683 ) ) ;
#29896=CARTESIAN_POINT ( 'NONE',  ( -3.834000099192893973, 2.652495916366584439, -25.46779765530001072 ) ) ;
#29926=CARTESIAN_POINT ( 'NONE',  ( 1.537204335059164872, 5.727607561491170785, -3.053410702900001716 ) ) ;
#29927=CARTESIAN_POINT ( 'NONE',  ( 1.771049722044198971, -6.234229536879996481, -21.29535708919999593 ) ) ;
#29940=CARTESIAN_POINT ( 'NONE',  ( -4.273751495587445604, 4.364932658710685587, -4.568732180600005854 ) ) ;
#29960=CARTESIAN_POINT ( 'NONE',  ( -0.6370991518874352666, 4.292107257743940529, -10.86772091660000150 ) ) ;
#30016=CARTESIAN_POINT ( 'NONE',  ( -6.074876045044606876, 0.8789665559579967757, -34.25783976329999092 ) ) ;
#30035=CARTESIAN_POINT ( 'NONE',  ( -4.600743226517092666, 1.661770424157335224, -0.6999999999999992895 ) ) ;
#30036=CARTESIAN_POINT ( 'NONE',  ( -5.478535709405480958, -2.209361269785813153, 0.002802565500000658849 ) ) ;
#30041=CARTESIAN_POINT ( 'NONE',  ( -4.363437395929424589, 0.1294788321584636748, -13.68304957890000750 ) ) ;
#30042=CARTESIAN_POINT ( 'NONE',  ( 3.155489075140828437, 3.034105443485042741, -35.32341724620001600 ) ) ;
#30070=CARTESIAN_POINT ( 'NONE',  ( 3.728365721074163197, -0.5735620887561410086, -35.69999999999999574 ) ) ;
#30084=CARTESIAN_POINT ( 'NONE',  ( -3.885731905334995684, 2.027028853511404272, -1.918764356300002305 ) ) ;
#30085=CARTESIAN_POINT ( 'NONE',  ( -4.663991843195165465, -3.413757688390889555, -18.27254627009999766 ) ) ;
#30100=CARTESIAN_POINT ( 'NONE',  ( -5.837703056366890131, -0.5751183411571159088, -1.146254077200002719 ) ) ;
#30121=PRODUCT_DEFINITION_CONTEXT ( 'detailed design', #3966, 'design' ) ;
#30123=CARTESIAN_POINT ( 'NONE',  ( 4.310466091822805268, 1.786666325167808544, -11.49261350019999739 ) ) ;
#30178=CARTESIAN_POINT ( 'NONE',  ( 3.996952828541906033, 3.843200228390037498, -36.32341724620000889 ) ) ;
#30195=CARTESIAN_POINT ( 'NONE',  ( -5.440024667461782037, 2.837840394948672351, -1.418764356299999418 ) ) ;
#30198=CARTESIAN_POINT ( 'NONE',  ( 1.526412975746457290, -4.524531468931415112, -16.20164732020000287 ) ) ;
#30199=CARTESIAN_POINT ( 'NONE',  ( -4.901082056047598279, -4.330235462250267453, -33.83447003409999354 ) ) ;
#30230=CARTESIAN_POINT ( 'NONE',  ( 1.169668886176895350, 3.927335417484261182, -35.70000000000000284 ) ) ;
#30237=CARTESIAN_POINT ( 'NONE',  ( 2.445722248254770026, -3.773326582131152573, -1.103439388299995549 ) ) ;
#30238=CARTESIAN_POINT ( 'NONE',  ( 5.195105410215491659, 3.969764343816663210, -23.36727430110000014 ) ) ;
#30257=CARTESIAN_POINT ( 'NONE',  ( 3.550610403408205329, -5.007233058897099021, -12.12388893670000201 ) ) ;
#30279=CARTESIAN_POINT ( 'NONE',  ( 4.945711323160860928, -2.526642934800090945, -10.91474735219999204 ) ) ;
#30309=B_SPLINE_CURVE_WITH_KNOTS ( 'NONE', 5,
 ( #28175, #11347, #18726, #22996, #30070, #30394 ),
 .UNSPECIFIED., .F., .F.,
 ( 6, 6 ),
 ( 0.000000000000000000, 2.893232387900000813 ),
 .UNSPECIFIED. ) ;
#30341=CARTESIAN_POINT ( 'NONE',  ( 0.07512830594655582617, -4.346272141329937888, -33.91110030500001216 ) ) ;
#30360=CARTESIAN_POINT ( 'NONE',  ( -2.825020644939634007, -4.425443225455641283, -0.6999999999999992895 ) ) ;
#30361=CARTESIAN_POINT ( 'NONE',  ( -3.510061880997908279, 5.032561185093348044, -1.027651354100003633 ) ) ;
#30364=CARTESIAN_POINT ( 'NONE',  ( 1.942707423728255778, -5.758494596869851989, -15.86414732020000784 ) ) ;
#30365=CARTESIAN_POINT ( 'NONE',  ( 3.123710955063051298, -2.074832491810060020, -35.95875473020000612 ) ) ;
#30394=CARTESIAN_POINT ( 'NONE',  ( 3.746497173757565413, -0.1670055334890632737, -35.69999999999999574 ) ) ;
#30407=CARTESIAN_POINT ( 'NONE',  ( -0.9973419271877559389, -5.413498265897602302, -4.525234013000000388 ) ) ;
#30408=CARTESIAN_POINT ( 'NONE',  ( -5.340187987486594068, -1.400932219821331870, -24.04656121680001135 ) ) ;
#30428=CARTESIAN_POINT ( 'NONE',  ( -4.555585884337687297, -4.059738318096004939, -24.84101932450000305 ) ) ;
#30448=CARTESIAN_POINT ( 'NONE',  ( -1.184025259985578948, -4.532227402022654061, -12.05022317840000845 ) ) ;
#30504=CARTESIAN_POINT ( 'NONE',  ( 4.051823674760409943, -0.6775361292690254000, -35.74517599850000948 ) ) ;
#30521=CARTESIAN_POINT ( 'NONE',  ( -6.505526340832360255, -0.4164809035307331930, -3.548838774899996995 ) ) ;
#30525=CARTESIAN_POINT ( 'NONE',  ( -3.057389860650357338, 5.459897439232808125, -16.67761783620000315 ) ) ;
#30526=CARTESIAN_POINT ( 'NONE',  ( 3.996952828541906033, 3.843200228390037498, -34.32341724620000889 ) ) ;
#30562=CARTESIAN_POINT ( 'NONE',  ( -0.7873752056533345201, -4.273814420472608511, -3.525234013000005717 ) ) ;
#30563=CARTESIAN_POINT ( 'NONE',  ( -3.253989917302559043, -2.899813084402115049, -24.84101932450000305 ) ) ;
#30580=CARTESIAN_POINT ( 'NONE',  ( 4.657610845611275252, 3.324676482552371581, -35.37908769469999726 ) ) ;
#30603=CARTESIAN_POINT ( 'NONE',  ( -4.335484423225056005, -2.064402852395420318, -12.03905742010000246 ) ) ;
#30674=CARTESIAN_POINT ( 'NONE',  ( -3.357947603668644199, 3.429589946161242242, -3.631232180600004966 ) ) ;
#30678=CARTESIAN_POINT ( 'NONE',  ( 2.326244606069572285, 3.379075471592549729, -17.71259163650000446 ) ) ;
#30679=CARTESIAN_POINT ( 'NONE',  ( 4.373195337096333013, -2.904765488536246387, -35.95875473020000612 ) ) ;
#30692=CARTESIAN_POINT ( 'NONE',  ( -0.4642112451548723873, -5.194573592496900538, -0.7000356040109552147 ) ) ;
#30712=CARTESIAN_POINT ( 'NONE',  ( 2.521631941452523229, 3.946033397249450125, -5.200967428500000267 ) ) ;
#30713=CARTESIAN_POINT ( 'NONE',  ( -4.637531673247329955, -1.216599033067103264, -24.10906121680000069 ) ) ;
#30744=CARTESIAN_POINT ( 'NONE',  ( 1.644581066898457955, -4.845992769441807013, -0.7000398998402457273 ) ) ;
#30749=CARTESIAN_POINT ( 'NONE',  ( 0.7763070146520680836, 4.277613328189620923, -14.02400681850000197 ) ) ;
#30759=FACE_OUTER_BOUND ( 'NONE', #22609, .T. ) ;
#30779=ORIENTED_EDGE ( 'NONE', *, *, #9801, .T. ) ;
#30823=CARTESIAN_POINT ( 'NONE',  ( -6.277996069133942925, 1.777976852108807737, -6.710827254899999872 ) ) ;
#30829=CARTESIAN_POINT ( 'NONE',  ( 2.946576500976501478, 4.280162264036399655, -18.21259163650000090 ) ) ;
#30847=CARTESIAN_POINT ( 'NONE',  ( -0.8587415393533248675, -5.153862915431827396, -0.7000227180819994510 ) ) ;
#30870=CARTESIAN_POINT ( 'NONE',  ( 3.530284718056032833, 5.524446756132658898, -5.200967428500000267 ) ) ;
#30871=CARTESIAN_POINT ( 'NONE',  ( -6.202057249109299342, 1.908294659314309305, -21.72289663400001203 ) ) ;
#30886=CARTESIAN_POINT ( 'NONE',  ( 3.430850994441077439, -5.010772104901466406, -27.13292313650000764 ) ) ;
#30906=CARTESIAN_POINT ( 'NONE',  ( 3.823514640232639206, -2.731196763342798484, -0.7000558027893447610 ) ) ;
#30909=CARTESIAN_POINT ( 'NONE',  ( 3.316815470610420924, 4.395877990916175371, -13.22796858840000134 ) ) ;
#30978=CARTESIAN_POINT ( 'NONE',  ( -4.932711197237716227, 1.396981812416056457, -6.373327254900004846 ) ) ;
#30983=CARTESIAN_POINT ( 'NONE',  ( -3.117834729128555971, -4.866792379758847709, -18.70544088820000184 ) ) ;
#31012=CARTESIAN_POINT ( 'NONE',  ( 0.3623765971425356724, 4.318009531214683783, -35.69999999999999574 ) ) ;
#31019=CARTESIAN_POINT ( 'NONE',  ( -3.010188847181571870, -5.300177381000955812, -6.685065142700001850 ) ) ;
#31020=CARTESIAN_POINT ( 'NONE',  ( 6.118976883090258667, 2.212479739890888197, -25.91249766019999967 ) ) ;
#31026=CARTESIAN_POINT ( 'NONE',  ( -3.052679639724400928, 3.117809041995142749, -4.568732180599999637 ) ) ;
#31037=CARTESIAN_POINT ( 'NONE',  ( -3.665401116828205463, 4.874126016103034864, -19.63064294430000345 ) ) ;
#31060=CARTESIAN_POINT ( 'NONE',  ( -4.180754675048084401, 1.217138862148065659, -15.80443125760000456 ) ) ;
#31096=CARTESIAN_POINT ( 'NONE',  ( 3.748453146079709697, -2.489798990173139437, -35.69999999999999574 ) ) ;
ENDSEC;
END-ISO-10303-21;
